ISO-10303-21;
HEADER;
/* Generated by software containing ST-Developer
 * from STEP Tools, Inc. (www.steptools.com) 
 */

FILE_DESCRIPTION(
/* description */ ('Pipe clamp stand with threaded column'),
/* implementation_level */ '2;1');

FILE_NAME(
/* name */ 'M24 adjustment nut (2).step',
/* time_stamp */ '2026-10-27T10:55:48-07:00',
/* author */ (''),
/* organization */ (''),
/* preprocessor_version */ 'ST-DEVELOPER v20.2',
/* originating_system */ 'Autodesk Translation Framework v15.17.0.0',
/* authorisation */ '');

FILE_SCHEMA (('AUTOMOTIVE_DESIGN { 1 0 10303 214 3 1 1 }'));
ENDSEC;

DATA;
#10=MECHANICAL_DESIGN_GEOMETRIC_PRESENTATION_REPRESENTATION('',(#769),#34433);
#213=B_SPLINE_SURFACE_WITH_KNOTS('',3,3,((#32106,#32107,#32108,#32109,#32110,
#32111,#32112,#32113,#32114,#32115,#32116,#32117,#32118,#32119,#32120,#32121,
#32122,#32123,#32124,#32125,#32126,#32127,#32128,#32129,#32130,#32131,#32132,
#32133,#32134,#32135,#32136,#32137,#32138,#32139,#32140,#32141,#32142,#32143,
#32144,#32145,#32146,#32147,#32148,#32149,#32150,#32151,#32152,#32153,#32154,
#32155,#32156,#32157,#32158,#32159,#32160,#32161,#32162,#32163,#32164),
(#32165,#32166,#32167,#32168,#32169,#32170,#32171,#32172,#32173,#32174,
#32175,#32176,#32177,#32178,#32179,#32180,#32181,#32182,#32183,#32184,#32185,
#32186,#32187,#32188,#32189,#32190,#32191,#32192,#32193,#32194,#32195,#32196,
#32197,#32198,#32199,#32200,#32201,#32202,#32203,#32204,#32205,#32206,#32207,
#32208,#32209,#32210,#32211,#32212,#32213,#32214,#32215,#32216,#32217,#32218,
#32219,#32220,#32221,#32222,#32223),(#32224,#32225,#32226,#32227,#32228,
#32229,#32230,#32231,#32232,#32233,#32234,#32235,#32236,#32237,#32238,#32239,
#32240,#32241,#32242,#32243,#32244,#32245,#32246,#32247,#32248,#32249,#32250,
#32251,#32252,#32253,#32254,#32255,#32256,#32257,#32258,#32259,#32260,#32261,
#32262,#32263,#32264,#32265,#32266,#32267,#32268,#32269,#32270,#32271,#32272,
#32273,#32274,#32275,#32276,#32277,#32278,#32279,#32280,#32281,#32282),
(#32283,#32284,#32285,#32286,#32287,#32288,#32289,#32290,#32291,#32292,
#32293,#32294,#32295,#32296,#32297,#32298,#32299,#32300,#32301,#32302,#32303,
#32304,#32305,#32306,#32307,#32308,#32309,#32310,#32311,#32312,#32313,#32314,
#32315,#32316,#32317,#32318,#32319,#32320,#32321,#32322,#32323,#32324,#32325,
#32326,#32327,#32328,#32329,#32330,#32331,#32332,#32333,#32334,#32335,#32336,
#32337,#32338,#32339,#32340,#32341)),.UNSPECIFIED.,.F.,.F.,.F.,(4,4),(4,
1,1,1,1,1,1,1,1,1,1,1,1,1,1,1,1,1,1,1,1,1,1,1,1,1,1,1,1,1,1,1,1,1,1,1,1,
1,1,1,1,1,1,1,1,1,1,1,1,1,1,1,1,1,1,1,4),(0.,0.193239135097767),(11.8520359647451,
12.3369705490203,12.8219051332956,13.3068397175709,13.7917743018462,14.2767088861214,
14.7616434703967,15.246578054672,15.7315126389473,16.2164472232226,16.7013818074978,
17.1863163917731,17.6712509760484,18.1561855603237,18.6411201445989,19.1260547288742,
19.6109893131495,20.0959238974248,20.5808584817,21.0657930659753,21.5507276502506,
22.0356622345259,22.5205968188012,23.0055314030764,23.4904659873517,23.975400571627,
24.4603351559023,24.9452697401775,25.4302043244528,25.9151389087281,26.4000734930034,
26.8850080772787,27.3699426615539,27.8548772458292,28.3398118301045,28.8247464143798,
29.309680998655,29.7946155829303,30.2795501672056,30.7644847514809,31.2494193357561,
31.7343539200314,32.2192885043067,32.704223088582,33.1891576728573,33.6740922571325,
34.1590268414078,34.6439614256831,35.1288960099584,35.6138305942336,36.0987651785089,
36.5836997627842,37.0686343470595,37.5535689313348,38.03850351561,38.5234380998853,
39.0083726841606),.UNSPECIFIED.);
#214=B_SPLINE_SURFACE_WITH_KNOTS('',3,3,((#32540,#32541,#32542,#32543,#32544,
#32545,#32546,#32547,#32548,#32549,#32550,#32551,#32552,#32553,#32554,#32555,
#32556,#32557,#32558,#32559,#32560,#32561,#32562,#32563,#32564,#32565,#32566,
#32567,#32568,#32569,#32570,#32571,#32572,#32573,#32574,#32575,#32576,#32577,
#32578,#32579,#32580,#32581,#32582,#32583,#32584,#32585,#32586,#32587,#32588,
#32589,#32590,#32591,#32592,#32593,#32594,#32595,#32596,#32597,#32598),
(#32599,#32600,#32601,#32602,#32603,#32604,#32605,#32606,#32607,#32608,
#32609,#32610,#32611,#32612,#32613,#32614,#32615,#32616,#32617,#32618,#32619,
#32620,#32621,#32622,#32623,#32624,#32625,#32626,#32627,#32628,#32629,#32630,
#32631,#32632,#32633,#32634,#32635,#32636,#32637,#32638,#32639,#32640,#32641,
#32642,#32643,#32644,#32645,#32646,#32647,#32648,#32649,#32650,#32651,#32652,
#32653,#32654,#32655,#32656,#32657),(#32658,#32659,#32660,#32661,#32662,
#32663,#32664,#32665,#32666,#32667,#32668,#32669,#32670,#32671,#32672,#32673,
#32674,#32675,#32676,#32677,#32678,#32679,#32680,#32681,#32682,#32683,#32684,
#32685,#32686,#32687,#32688,#32689,#32690,#32691,#32692,#32693,#32694,#32695,
#32696,#32697,#32698,#32699,#32700,#32701,#32702,#32703,#32704,#32705,#32706,
#32707,#32708,#32709,#32710,#32711,#32712,#32713,#32714,#32715,#32716),
(#32717,#32718,#32719,#32720,#32721,#32722,#32723,#32724,#32725,#32726,
#32727,#32728,#32729,#32730,#32731,#32732,#32733,#32734,#32735,#32736,#32737,
#32738,#32739,#32740,#32741,#32742,#32743,#32744,#32745,#32746,#32747,#32748,
#32749,#32750,#32751,#32752,#32753,#32754,#32755,#32756,#32757,#32758,#32759,
#32760,#32761,#32762,#32763,#32764,#32765,#32766,#32767,#32768,#32769,#32770,
#32771,#32772,#32773,#32774,#32775)),.UNSPECIFIED.,.F.,.F.,.F.,(4,4),(4,
1,1,1,1,1,1,1,1,1,1,1,1,1,1,1,1,1,1,1,1,1,1,1,1,1,1,1,1,1,1,1,1,1,1,1,1,
1,1,1,1,1,1,1,1,1,1,1,1,1,1,1,1,1,1,1,4),(0.,0.193239135097767),(14.398702426866,
14.8836370111413,15.3685715954165,15.8535061796918,16.3384407639671,16.8233753482424,
17.3083099325176,17.7932445167929,18.2781791010682,18.7631136853435,19.2480482696188,
19.732982853894,20.2179174381693,20.7028520224446,21.1877866067199,21.6727211909951,
22.1576557752704,22.6425903595457,23.127524943821,23.6124595280962,24.0973941123715,
24.5823286966468,25.0672632809221,25.5521978651974,26.0371324494726,26.5220670337479,
27.0070016180232,27.4919362022985,27.9768707865737,28.461805370849,28.9467399551243,
29.4316745393996,29.9166091236749,30.4015437079501,30.8864782922254,31.3714128765007,
31.856347460776,32.3412820450512,32.8262166293265,33.3111512136018,33.7960857978771,
34.2810203821523,34.7659549664276,35.2508895507029,35.7358241349782,36.2207587192535,
36.7056933035287,37.190627887804,37.6755624720793,38.1604970563546,38.6454316406299,
39.1303662249051,39.6153008091804,40.1002353934557,40.585169977731,41.0701045620062,
41.5550391462815),.UNSPECIFIED.);
#649=B_SPLINE_CURVE_WITH_KNOTS('',3,(#31664,#31665,#31666,#31667,#31668,
#31669,#31670),.UNSPECIFIED.,.F.,.F.,(4,3,4),(26.4420020698013,26.6714021351403,
27.1563367194155),.UNSPECIFIED.);
#650=B_SPLINE_CURVE_WITH_KNOTS('',3,(#31673,#31674,#31675,#31676,#31677,
#31678,#31679,#31680,#31681,#31682,#31683,#31684,#31685,#31686,#31687,#31688,
#31689,#31690,#31691),.UNSPECIFIED.,.F.,.F.,(4,3,3,3,3,3,4),(-25.1327412287182,
-24.7316637980391,-24.2467292137639,-23.7617946294886,-23.2768600452133,
-22.791925460938,-22.7054832247427),.UNSPECIFIED.);
#651=B_SPLINE_CURVE_WITH_KNOTS('',3,(#31696,#31697,#31698,#31699,#31700,
#31701,#31702,#31703,#31704,#31705,#31706,#31707,#31708,#31709,#31710,#31711,
#31712,#31713,#31714,#31715,#31716,#31717,#31718,#31719,#31720,#31721,#31722,
#31723,#31724,#31725,#31726,#31727,#31728,#31729,#31730,#31731,#31732,#31733,
#31734,#31735,#31736,#31737,#31738),.UNSPECIFIED.,.F.,.F.,(4,3,3,3,3,3,
3,3,3,3,3,3,3,3,4),(20.1588167626218,20.3672525395616,20.8521871238369,
21.3371217081122,21.8220562923875,22.3069908766628,22.791925460938,23.2768600452133,
23.7617946294886,24.2467292137639,24.7316637980392,25.2165983823144,25.7015329665897,
26.186467550865,26.4420020698013),.UNSPECIFIED.);
#652=B_SPLINE_CURVE_WITH_KNOTS('',3,(#31739,#31740,#31741,#31742,#31743,
#31744,#31745,#31746,#31747,#31748,#31749,#31750,#31751,#31752,#31753,#31754,
#31755,#31756,#31757,#31758,#31759,#31760,#31761,#31762,#31763,#31764,#31765,
#31766,#31767,#31768,#31769,#31770,#31771,#31772,#31773,#31774,#31775,#31776,
#31777,#31778,#31779,#31780,#31781),.UNSPECIFIED.,.F.,.F.,(4,3,3,3,3,3,
3,3,3,3,3,3,3,3,4),(-22.7054832247427,-22.3069908766628,-21.8220562923875,
-21.3371217081122,-20.8521871238369,-20.3672525395616,-19.8823179552864,
-19.3973833710111,-18.9124487867358,-18.4275142024605,-17.9425796181853,
-17.45764503391,-16.9727104496347,-16.4877758653594,-16.4222979175631),
 .UNSPECIFIED.);
#653=B_SPLINE_CURVE_WITH_KNOTS('',3,(#31786,#31787,#31788,#31789,#31790,
#31791,#31792,#31793,#31794,#31795,#31796,#31797,#31798,#31799,#31800,#31801,
#31802,#31803,#31804,#31805,#31806,#31807,#31808,#31809,#31810,#31811,#31812,
#31813,#31814,#31815,#31816,#31817,#31818,#31819,#31820,#31821,#31822,#31823,
#31824,#31825,#31826,#31827,#31828),.UNSPECIFIED.,.F.,.F.,(4,3,3,3,3,3,
3,3,3,3,3,3,3,3,4),(13.8756314554422,14.063102943983,14.5480375282583,15.0329721125336,
15.5179066968089,16.0028412810842,16.4877758653594,16.9727104496347,17.45764503391,
17.9425796181853,18.4275142024605,18.9124487867358,19.3973833710111,19.8823179552864,
20.1588167626218),.UNSPECIFIED.);
#654=B_SPLINE_CURVE_WITH_KNOTS('',3,(#31829,#31830,#31831,#31832,#31833,
#31834,#31835,#31836,#31837,#31838,#31839,#31840,#31841,#31842,#31843,#31844,
#31845,#31846,#31847,#31848,#31849,#31850,#31851,#31852,#31853,#31854,#31855,
#31856,#31857,#31858,#31859,#31860,#31861,#31862,#31863,#31864,#31865,#31866,
#31867,#31868,#31869,#31870,#31871),.UNSPECIFIED.,.F.,.F.,(4,3,3,3,3,3,
3,3,3,3,3,3,3,3,4),(-16.4222979175631,-16.0028412810841,-15.5179066968089,
-15.0329721125336,-14.5480375282583,-14.063102943983,-13.5781683597078,
-13.0932337754325,-12.6082991911572,-12.1233646068819,-11.6384300226067,
-11.1534954383314,-10.6685608540561,-10.1836262697808,-10.1391126103835),
 .UNSPECIFIED.);
#655=B_SPLINE_CURVE_WITH_KNOTS('',3,(#31877,#31878,#31879,#31880,#31881,
#31882,#31883,#31884,#31885,#31886,#31887,#31888,#31889,#31890,#31891,#31892,
#31893,#31894,#31895,#31896,#31897,#31898,#31899,#31900,#31901),
 .UNSPECIFIED.,.F.,.F.,(4,3,3,3,3,3,3,3,4),(-3.8559273032039,-3.39454208992694,
-2.90960750565166,-2.42467292137639,-1.93973833710111,-1.45480375282583,
-0.969869168550556,-0.484934584275276,0.),.UNSPECIFIED.);
#656=B_SPLINE_CURVE_WITH_KNOTS('',3,(#31904,#31905,#31906,#31907,#31908,
#31909,#31910,#31911,#31912,#31913,#31914,#31915,#31916,#31917,#31918,#31919,
#31920,#31921,#31922,#31923,#31924,#31925,#31926,#31927,#31928,#31929,#31930,
#31931,#31932,#31933,#31934,#31935,#31936,#31937,#31938,#31939,#31940),
 .UNSPECIFIED.,.F.,.F.,(4,3,3,3,3,3,3,3,3,3,3,3,4),(2.02359549069725,2.42467292137639,
2.90960750565167,3.39454208992694,3.87947667420222,4.3644112584775,4.84934584275277,
5.33428042702805,5.81921501130333,6.30414959557861,6.78908417985388,7.27401876412916,
7.59244614826257),.UNSPECIFIED.);
#657=B_SPLINE_CURVE_WITH_KNOTS('',3,(#31946,#31947,#31948,#31949,#31950,
#31951,#31952,#31953,#31954,#31955,#31956,#31957,#31958),.UNSPECIFIED.,
 .F.,.F.,(4,1,1,1,1,1,1,1,1,1,4),(34.5575191894877,34.6439614256831,35.1288960099584,
35.6138305942336,36.0987651785089,36.5836997627842,37.0686343470595,37.5535689313348,
38.03850351561,38.5234380998853,39.0083726841606),.UNSPECIFIED.);
#658=B_SPLINE_CURVE_WITH_KNOTS('',3,(#31961,#31962,#31963,#31964,#31965,
#31966,#31967,#31968,#31969,#31970,#31971,#31972,#31973,#31974),
 .UNSPECIFIED.,.F.,.F.,(4,1,1,1,1,1,1,1,1,1,1,4),(34.5575191894877,34.7659549664276,
35.2508895507029,35.7358241349782,36.2207587192535,36.7056933035287,37.190627887804,
37.6755624720793,38.1604970563546,38.6454316406299,39.1303662249051,39.5314436555842),
 .UNSPECIFIED.);
#659=B_SPLINE_CURVE_WITH_KNOTS('',3,(#31979,#31980,#31981,#31982,#31983,
#31984,#31985,#31986,#31987,#31988,#31989,#31990,#31991,#31992,#31993,#31994,
#31995),.UNSPECIFIED.,.F.,.F.,(4,1,1,1,1,1,1,1,1,1,1,1,1,1,4),(28.2743338823082,
28.3398118301045,28.8247464143798,29.309680998655,29.7946155829303,30.2795501672056,
30.7644847514809,31.2494193357561,31.7343539200314,32.2192885043067,32.704223088582,
33.1891576728573,33.6740922571325,34.1590268414078,34.5575191894877),
 .UNSPECIFIED.);
#660=B_SPLINE_CURVE_WITH_KNOTS('',3,(#31996,#31997,#31998,#31999,#32000,
#32001,#32002,#32003,#32004,#32005,#32006,#32007,#32008,#32009,#32010,#32011,
#32012),.UNSPECIFIED.,.F.,.F.,(4,1,1,1,1,1,1,1,1,1,1,1,1,1,4),(28.2743338823082,
28.461805370849,28.9467399551243,29.4316745393996,29.9166091236749,30.4015437079501,
30.8864782922254,31.3714128765007,31.856347460776,32.3412820450512,32.8262166293265,
33.3111512136018,33.7960857978771,34.2810203821523,34.5575191894877),
 .UNSPECIFIED.);
#661=B_SPLINE_CURVE_WITH_KNOTS('',3,(#32017,#32018,#32019,#32020,#32021,
#32022,#32023,#32024,#32025,#32026,#32027,#32028,#32029,#32030,#32031,#32032,
#32033),.UNSPECIFIED.,.F.,.F.,(4,1,1,1,1,1,1,1,1,1,1,1,1,1,4),(21.9911485751286,
22.0356622345259,22.5205968188012,23.0055314030764,23.4904659873517,23.975400571627,
24.4603351559023,24.9452697401775,25.4302043244528,25.9151389087281,26.4000734930034,
26.8850080772787,27.3699426615539,27.8548772458292,28.2743338823082),
 .UNSPECIFIED.);
#662=B_SPLINE_CURVE_WITH_KNOTS('',3,(#32034,#32035,#32036,#32037,#32038,
#32039,#32040,#32041,#32042,#32043,#32044,#32045,#32046,#32047,#32048,#32049,
#32050),.UNSPECIFIED.,.F.,.F.,(4,1,1,1,1,1,1,1,1,1,1,1,1,1,4),(21.9911485751286,
22.1576557752704,22.6425903595457,23.127524943821,23.6124595280962,24.0973941123715,
24.5823286966468,25.0672632809221,25.5521978651974,26.0371324494726,26.5220670337479,
27.0070016180232,27.4919362022985,27.9768707865737,28.2743338823082),
 .UNSPECIFIED.);
#663=B_SPLINE_CURVE_WITH_KNOTS('',3,(#32056,#32057,#32058,#32059,#32060,
#32061),.UNSPECIFIED.,.F.,.F.,(4,1,1,4),(14.398702426866,14.8836370111413,
15.3685715954165,15.707963267949),.UNSPECIFIED.);
#664=B_SPLINE_CURVE_WITH_KNOTS('',3,(#32064,#32065,#32066,#32067,#32068,
#32069,#32070),.UNSPECIFIED.,.F.,.F.,(4,1,1,1,4),(13.8756314554423,14.2767088861214,
14.7616434703967,15.246578054672,15.707963267949),.UNSPECIFIED.);
#665=B_SPLINE_CURVE_WITH_KNOTS('',3,(#32072,#32073,#32074,#32075,#32076,
#32077,#32078,#32079,#32080,#32081,#32082,#32083,#32084,#32085,#32086,#32087,
#32088),.UNSPECIFIED.,.F.,.F.,(4,1,1,1,1,1,1,1,1,1,1,1,1,1,4),(15.707963267949,
15.7315126389473,16.2164472232226,16.7013818074978,17.1863163917731,17.6712509760484,
18.1561855603237,18.6411201445989,19.1260547288742,19.6109893131495,20.0959238974248,
20.5808584817,21.0657930659753,21.5507276502506,21.9911485751286),
 .UNSPECIFIED.);
#666=B_SPLINE_CURVE_WITH_KNOTS('',3,(#32089,#32090,#32091,#32092,#32093,
#32094,#32095,#32096,#32097,#32098,#32099,#32100,#32101,#32102,#32103,#32104,
#32105),.UNSPECIFIED.,.F.,.F.,(4,1,1,1,1,1,1,1,1,1,1,1,1,1,4),(15.707963267949,
15.8535061796918,16.3384407639671,16.8233753482424,17.3083099325176,17.7932445167929,
18.2781791010682,18.7631136853435,19.2480482696188,19.732982853894,20.2179174381693,
20.7028520224446,21.1877866067199,21.6727211909951,21.9911485751286),
 .UNSPECIFIED.);
#667=B_SPLINE_CURVE_WITH_KNOTS('',3,(#32342,#32343,#32344,#32345,#32346,
#32347,#32348,#32349,#32350,#32351,#32352,#32353,#32354,#32355,#32356,#32357,
#32358,#32359,#32360,#32361,#32362,#32363,#32364,#32365,#32366,#32367,#32368,
#32369,#32370,#32371,#32372,#32373,#32374,#32375,#32376,#32377,#32378,#32379,
#32380,#32381,#32382,#32383,#32384,#32385,#32386,#32387,#32388,#32389,#32390,
#32391,#32392,#32393,#32394,#32395,#32396,#32397,#32398,#32399,#32400,#32401,
#32402,#32403,#32404,#32405,#32406,#32407,#32408,#32409,#32410,#32411,#32412,
#32413,#32414,#32415,#32416,#32417,#32418,#32419,#32420),.UNSPECIFIED.,
 .F.,.F.,(4,3,3,3,3,3,3,3,3,3,3,3,3,3,3,3,3,3,3,3,3,3,3,3,3,3,4),(0.,0.152215941592882,
0.304359238378302,0.44417026434153,0.471986524584209,0.583981290304758,
0.733405333521443,0.837349616957177,0.892796925719252,0.921011414368794,
0.95123360439561,1.09712049653845,1.14918246726438,1.28571136325169,1.34308244168001,
1.37129901391245,1.51452711558388,1.6561323669284,1.69529805121364,1.76334987370452,
1.79789372311875,1.82919290943268,1.96987779531733,2.04822506388956,2.08147563082119,
2.22116640322435,2.31010750305866),.UNSPECIFIED.);
#668=B_SPLINE_CURVE_WITH_KNOTS('',3,(#32421,#32422,#32423,#32424,#32425,
#32426,#32427,#32428,#32429,#32430,#32431,#32432,#32433,#32434,#32435,#32436,
#32437,#32438,#32439,#32440,#32441,#32442,#32443,#32444,#32445,#32446,#32447,
#32448,#32449,#32450,#32451,#32452,#32453,#32454,#32455,#32456,#32457,#32458,
#32459,#32460,#32461,#32462,#32463,#32464,#32465,#32466,#32467,#32468,#32469,
#32470,#32471,#32472,#32473,#32474,#32475,#32476,#32477,#32478,#32479,#32480,
#32481,#32482,#32483,#32484,#32485,#32486,#32487,#32488,#32489,#32490,#32491,
#32492,#32493,#32494,#32495,#32496),.UNSPECIFIED.,.F.,.F.,(4,3,3,3,3,3,
3,3,3,3,3,3,3,3,3,3,3,3,3,3,3,3,3,3,3,4),(0.,0.13694288511905,0.275839534909346,
0.398831870824263,0.43364457290582,0.521824206739181,0.663226502332769,
0.763151450184378,0.825068371201986,0.861088466872379,1.00600743409727,
1.06292629373921,1.20295657612767,1.26303420520301,1.30095884525044,1.44786376844848,
1.59610976549603,1.62304742329305,1.69648826291636,1.73120219323328,1.76336665553203,
1.91360293601108,1.99760347404716,2.04132626333146,2.20106314648734,2.30292298333801),
 .UNSPECIFIED.);
#669=B_SPLINE_CURVE_WITH_KNOTS('',3,(#32497,#32498,#32499,#32500,#32501,
#32502,#32503,#32504,#32505,#32506,#32507,#32508,#32509,#32510,#32511,#32512,
#32513,#32514,#32515,#32516,#32517,#32518,#32519,#32520,#32521,#32522,#32523,
#32524,#32525,#32526,#32527,#32528,#32529,#32530,#32531,#32532,#32533,#32534,
#32535,#32536,#32537,#32538,#32539),.UNSPECIFIED.,.F.,.F.,(4,3,3,3,3,3,
3,3,3,3,3,3,3,3,4),(-10.1391126103835,-9.69869168550554,-9.21375710123027,
-8.72882251695499,-8.24388793267971,-7.75895334840444,-7.27401876412916,
-6.78908417985388,-6.3041495955786,-5.81921501130332,-5.33428042702805,
-4.84934584275277,-4.3644112584775,-3.87947667420222,-3.8559273032039),
 .UNSPECIFIED.);
#670=B_SPLINE_CURVE_WITH_KNOTS('',3,(#32776,#32777,#32778,#32779,#32780,
#32781,#32782,#32783,#32784,#32785,#32786,#32787,#32788,#32789,#32790,#32791,
#32792,#32793,#32794,#32795,#32796,#32797,#32798,#32799,#32800,#32801,#32802,
#32803,#32804,#32805,#32806,#32807,#32808,#32809,#32810,#32811,#32812,#32813,
#32814,#32815,#32816,#32817,#32818,#32819,#32820,#32821,#32822,#32823,#32824,
#32825,#32826,#32827,#32828,#32829,#32830,#32831,#32832,#32833,#32834,#32835,
#32836,#32837,#32838,#32839,#32840,#32841,#32842,#32843,#32844,#32845,#32846,
#32847,#32848,#32849,#32850,#32851),.UNSPECIFIED.,.F.,.F.,(4,3,3,3,3,3,
3,3,3,3,3,3,3,3,3,3,3,3,3,3,3,3,3,3,3,4),(0.,0.136942783675313,0.275839386965687,
0.398831796852438,0.433644559362179,0.52182420673919,0.663226551512937,
0.763151487069502,0.825068482010607,0.861088472748197,1.00600747520934,
1.0629262937392,1.20295657612766,1.2630342054286,1.30095884559252,1.4478637544197,
1.59610974893898,1.62304742329305,1.69648826363017,1.73120220104301,1.76336665734949,
1.91360293688396,1.99760347568968,2.04132626433107,2.20106314648737,2.30292298333823),
 .UNSPECIFIED.);
#671=B_SPLINE_CURVE_WITH_KNOTS('',3,(#32852,#32853,#32854,#32855,#32856,
#32857,#32858,#32859,#32860,#32861,#32862,#32863,#32864,#32865,#32866,#32867,
#32868,#32869,#32870,#32871,#32872,#32873,#32874,#32875,#32876,#32877,#32878,
#32879,#32880,#32881,#32882,#32883,#32884,#32885,#32886,#32887,#32888,#32889,
#32890,#32891,#32892,#32893,#32894),.UNSPECIFIED.,.F.,.F.,(4,3,3,3,3,3,
3,3,3,3,3,3,3,3,4),(7.59244614826257,7.75895334840444,8.24388793267972,
8.728822516955,9.21375710123027,9.69869168550555,10.1836262697808,10.6685608540561,
11.1534954383314,11.6384300226067,12.1233646068819,12.6082991911572,13.0932337754325,
13.5781683597078,13.8756314554422),.UNSPECIFIED.);
#672=B_SPLINE_CURVE_WITH_KNOTS('',3,(#32895,#32896,#32897,#32898,#32899,
#32900,#32901,#32902,#32903,#32904,#32905,#32906,#32907,#32908,#32909,#32910,
#32911,#32912,#32913,#32914,#32915,#32916,#32917,#32918,#32919,#32920,#32921,
#32922,#32923,#32924,#32925,#32926,#32927,#32928,#32929,#32930,#32931,#32932,
#32933,#32934,#32935,#32936,#32937,#32938,#32939,#32940,#32941,#32942,#32943,
#32944,#32945,#32946,#32947,#32948,#32949,#32950,#32951,#32952,#32953,#32954,
#32955,#32956,#32957,#32958,#32959,#32960,#32961,#32962,#32963,#32964,#32965,
#32966,#32967,#32968,#32969,#32970,#32971,#32972,#32973),.UNSPECIFIED.,
 .F.,.F.,(4,3,3,3,3,3,3,3,3,3,3,3,3,3,3,3,3,3,3,3,3,3,3,3,3,3,4),(0.,0.152215902191206,
0.304359225867899,0.444170258086332,0.471986521031257,0.583981290304766,
0.733405339782993,0.837349621653341,0.892796945580561,0.921011356266073,
0.95123359785535,1.09712048593541,1.14918246726438,1.28571136325169,1.34308244436525,
1.37129901598247,1.51452711514042,1.65613236306049,1.69529805121362,1.76334987454827,
1.79789373174083,1.82919291148127,1.9698777983055,2.04822506867616,2.08147563558465,
2.2211664032244,2.31010750305872),.UNSPECIFIED.);
#717=SHAPE_REPRESENTATION_RELATIONSHIP('SRR','None',#34562,#739);
#739=ADVANCED_BREP_SHAPE_REPRESENTATION('',(#797),#34430);
#769=STYLED_ITEM('',(#34750),#797);
#797=MANIFOLD_SOLID_BREP('Body1',#8798);
#853=FACE_BOUND('',#2044,.T.);
#854=FACE_BOUND('',#2053,.T.);
#1028=PLANE('',#9685);
#1029=PLANE('',#9687);
#1030=PLANE('',#9688);
#1031=PLANE('',#9689);
#1032=PLANE('',#9690);
#1033=PLANE('',#9691);
#1034=PLANE('',#9692);
#1035=PLANE('',#9693);
#1491=FACE_OUTER_BOUND('',#2032,.T.);
#1492=FACE_OUTER_BOUND('',#2033,.T.);
#1493=FACE_OUTER_BOUND('',#2034,.T.);
#1494=FACE_OUTER_BOUND('',#2035,.T.);
#1495=FACE_OUTER_BOUND('',#2036,.T.);
#1496=FACE_OUTER_BOUND('',#2037,.T.);
#1497=FACE_OUTER_BOUND('',#2038,.T.);
#1498=FACE_OUTER_BOUND('',#2039,.T.);
#1499=FACE_OUTER_BOUND('',#2040,.T.);
#1500=FACE_OUTER_BOUND('',#2041,.T.);
#1501=FACE_OUTER_BOUND('',#2042,.T.);
#1502=FACE_OUTER_BOUND('',#2043,.T.);
#1503=FACE_OUTER_BOUND('',#2045,.T.);
#1504=FACE_OUTER_BOUND('',#2046,.T.);
#1505=FACE_OUTER_BOUND('',#2047,.T.);
#1506=FACE_OUTER_BOUND('',#2048,.T.);
#1507=FACE_OUTER_BOUND('',#2049,.T.);
#1508=FACE_OUTER_BOUND('',#2050,.T.);
#1509=FACE_OUTER_BOUND('',#2051,.T.);
#1510=FACE_OUTER_BOUND('',#2052,.T.);
#2032=EDGE_LOOP('',(#7783,#7784,#7785,#7786));
#2033=EDGE_LOOP('',(#7787,#7788,#7789,#7790));
#2034=EDGE_LOOP('',(#7791,#7792,#7793,#7794));
#2035=EDGE_LOOP('',(#7795,#7796,#7797,#7798));
#2036=EDGE_LOOP('',(#7799,#7800,#7801,#7802));
#2037=EDGE_LOOP('',(#7803,#7804,#7805,#7806));
#2038=EDGE_LOOP('',(#7807,#7808,#7809,#7810));
#2039=EDGE_LOOP('',(#7811,#7812,#7813,#7814));
#2040=EDGE_LOOP('',(#7815,#7816,#7817,#7818));
#2041=EDGE_LOOP('',(#7819,#7820,#7821,#7822,#7823,#7824,#7825,#7826,#7827,
#7828,#7829,#7830));
#2042=EDGE_LOOP('',(#7831,#7832,#7833,#7834,#7835,#7836,#7837,#7838,#7839,
#7840,#7841,#7842));
#2043=EDGE_LOOP('',(#7843,#7844,#7845,#7846,#7847,#7848));
#2044=EDGE_LOOP('',(#7849,#7850,#7851,#7852));
#2045=EDGE_LOOP('',(#7853,#7854,#7855,#7856));
#2046=EDGE_LOOP('',(#7857,#7858,#7859,#7860));
#2047=EDGE_LOOP('',(#7861,#7862,#7863,#7864));
#2048=EDGE_LOOP('',(#7865,#7866,#7867,#7868));
#2049=EDGE_LOOP('',(#7869,#7870,#7871,#7872));
#2050=EDGE_LOOP('',(#7873,#7874,#7875,#7876));
#2051=EDGE_LOOP('',(#7877,#7878,#7879,#7880));
#2052=EDGE_LOOP('',(#7881,#7882,#7883,#7884,#7885,#7886));
#2053=EDGE_LOOP('',(#7887,#7888,#7889,#7890));
#2641=LINE('',#31662,#3258);
#2642=LINE('',#31695,#3259);
#2643=LINE('',#31785,#3260);
#2644=LINE('',#31875,#3261);
#2645=LINE('',#31944,#3262);
#2646=LINE('',#31978,#3263);
#2647=LINE('',#32016,#3264);
#2648=LINE('',#32054,#3265);
#2649=LINE('',#32977,#3266);
#2650=LINE('',#32979,#3267);
#2651=LINE('',#32981,#3268);
#2652=LINE('',#32983,#3269);
#2653=LINE('',#32985,#3270);
#2654=LINE('',#32986,#3271);
#2655=LINE('',#32991,#3272);
#2656=LINE('',#32992,#3273);
#2657=LINE('',#32993,#3274);
#2658=LINE('',#32996,#3275);
#2659=LINE('',#32997,#3276);
#2660=LINE('',#33000,#3277);
#2661=LINE('',#33001,#3278);
#2662=LINE('',#33004,#3279);
#2663=LINE('',#33005,#3280);
#2664=LINE('',#33008,#3281);
#2665=LINE('',#33009,#3282);
#2666=LINE('',#33011,#3283);
#3258=VECTOR('',#11550,1.05);
#3259=VECTOR('',#11555,1.05);
#3260=VECTOR('',#11558,1.05);
#3261=VECTOR('',#11561,1.05);
#3262=VECTOR('',#11566,1.21745);
#3263=VECTOR('',#11571,1.21745);
#3264=VECTOR('',#11574,1.21745);
#3265=VECTOR('',#11577,1.21745);
#3266=VECTOR('',#11584,1.);
#3267=VECTOR('',#11585,1.);
#3268=VECTOR('',#11586,1.);
#3269=VECTOR('',#11587,1.);
#3270=VECTOR('',#11588,1.);
#3271=VECTOR('',#11589,1.);
#3272=VECTOR('',#11594,1.);
#3273=VECTOR('',#11595,1.);
#3274=VECTOR('',#11596,1.);
#3275=VECTOR('',#11599,1.);
#3276=VECTOR('',#11600,1.);
#3277=VECTOR('',#11603,1.);
#3278=VECTOR('',#11604,1.);
#3279=VECTOR('',#11607,1.);
#3280=VECTOR('',#11608,1.);
#3281=VECTOR('',#11611,1.);
#3282=VECTOR('',#11612,1.);
#3283=VECTOR('',#11615,1.);
#3436=CIRCLE('',#9673,1.0501);
#3437=CIRCLE('',#9677,1.0501);
#3438=CIRCLE('',#9679,1.21745);
#3439=CIRCLE('',#9683,1.21745);
#4198=VERTEX_POINT('',#31660);
#4199=VERTEX_POINT('',#31661);
#4200=VERTEX_POINT('',#31663);
#4201=VERTEX_POINT('',#31671);
#4202=VERTEX_POINT('',#31693);
#4203=VERTEX_POINT('',#31694);
#4204=VERTEX_POINT('',#31783);
#4205=VERTEX_POINT('',#31784);
#4206=VERTEX_POINT('',#31873);
#4207=VERTEX_POINT('',#31874);
#4208=VERTEX_POINT('',#31876);
#4209=VERTEX_POINT('',#31902);
#4210=VERTEX_POINT('',#31942);
#4211=VERTEX_POINT('',#31943);
#4212=VERTEX_POINT('',#31945);
#4213=VERTEX_POINT('',#31959);
#4214=VERTEX_POINT('',#31976);
#4215=VERTEX_POINT('',#31977);
#4216=VERTEX_POINT('',#32014);
#4217=VERTEX_POINT('',#32015);
#4218=VERTEX_POINT('',#32052);
#4219=VERTEX_POINT('',#32053);
#4220=VERTEX_POINT('',#32055);
#4221=VERTEX_POINT('',#32062);
#4222=VERTEX_POINT('',#32975);
#4223=VERTEX_POINT('',#32976);
#4224=VERTEX_POINT('',#32978);
#4225=VERTEX_POINT('',#32980);
#4226=VERTEX_POINT('',#32982);
#4227=VERTEX_POINT('',#32984);
#4228=VERTEX_POINT('',#32989);
#4229=VERTEX_POINT('',#32990);
#4230=VERTEX_POINT('',#32995);
#4231=VERTEX_POINT('',#32999);
#4232=VERTEX_POINT('',#33003);
#4233=VERTEX_POINT('',#33007);
#5405=EDGE_CURVE('',#4198,#4199,#2641,.T.);
#5406=EDGE_CURVE('',#4199,#4200,#649,.T.);
#5407=EDGE_CURVE('',#4201,#4200,#3436,.T.);
#5408=EDGE_CURVE('',#4201,#4198,#650,.T.);
#5409=EDGE_CURVE('',#4202,#4203,#2642,.T.);
#5410=EDGE_CURVE('',#4203,#4199,#651,.T.);
#5411=EDGE_CURVE('',#4198,#4202,#652,.T.);
#5412=EDGE_CURVE('',#4204,#4205,#2643,.T.);
#5413=EDGE_CURVE('',#4205,#4203,#653,.T.);
#5414=EDGE_CURVE('',#4202,#4204,#654,.T.);
#5415=EDGE_CURVE('',#4206,#4207,#2644,.T.);
#5416=EDGE_CURVE('',#4206,#4208,#655,.T.);
#5417=EDGE_CURVE('',#4209,#4208,#3437,.F.);
#5418=EDGE_CURVE('',#4209,#4207,#656,.T.);
#5419=EDGE_CURVE('',#4210,#4211,#2645,.T.);
#5420=EDGE_CURVE('',#4211,#4212,#657,.T.);
#5421=EDGE_CURVE('',#4213,#4212,#3438,.T.);
#5422=EDGE_CURVE('',#4210,#4213,#658,.T.);
#5423=EDGE_CURVE('',#4214,#4215,#2646,.T.);
#5424=EDGE_CURVE('',#4215,#4211,#659,.T.);
#5425=EDGE_CURVE('',#4214,#4210,#660,.T.);
#5426=EDGE_CURVE('',#4216,#4217,#2647,.T.);
#5427=EDGE_CURVE('',#4217,#4215,#661,.T.);
#5428=EDGE_CURVE('',#4216,#4214,#662,.T.);
#5429=EDGE_CURVE('',#4218,#4219,#2648,.T.);
#5430=EDGE_CURVE('',#4220,#4218,#663,.T.);
#5431=EDGE_CURVE('',#4221,#4220,#3439,.T.);
#5432=EDGE_CURVE('',#4221,#4219,#664,.T.);
#5433=EDGE_CURVE('',#4219,#4217,#665,.T.);
#5434=EDGE_CURVE('',#4218,#4216,#666,.T.);
#5435=EDGE_CURVE('',#4212,#4201,#667,.T.);
#5436=EDGE_CURVE('',#4208,#4221,#668,.T.);
#5437=EDGE_CURVE('',#4204,#4206,#669,.T.);
#5438=EDGE_CURVE('',#4200,#4213,#670,.T.);
#5439=EDGE_CURVE('',#4207,#4205,#671,.T.);
#5440=EDGE_CURVE('',#4220,#4209,#672,.T.);
#5441=EDGE_CURVE('',#4222,#4223,#2649,.T.);
#5442=EDGE_CURVE('',#4223,#4224,#2650,.T.);
#5443=EDGE_CURVE('',#4224,#4225,#2651,.T.);
#5444=EDGE_CURVE('',#4225,#4226,#2652,.T.);
#5445=EDGE_CURVE('',#4226,#4227,#2653,.T.);
#5446=EDGE_CURVE('',#4227,#4222,#2654,.T.);
#5447=EDGE_CURVE('',#4228,#4229,#2655,.T.);
#5448=EDGE_CURVE('',#4229,#4222,#2656,.T.);
#5449=EDGE_CURVE('',#4228,#4227,#2657,.T.);
#5450=EDGE_CURVE('',#4230,#4228,#2658,.T.);
#5451=EDGE_CURVE('',#4230,#4226,#2659,.T.);
#5452=EDGE_CURVE('',#4231,#4230,#2660,.T.);
#5453=EDGE_CURVE('',#4231,#4225,#2661,.T.);
#5454=EDGE_CURVE('',#4232,#4231,#2662,.T.);
#5455=EDGE_CURVE('',#4232,#4224,#2663,.T.);
#5456=EDGE_CURVE('',#4233,#4232,#2664,.T.);
#5457=EDGE_CURVE('',#4233,#4223,#2665,.T.);
#5458=EDGE_CURVE('',#4229,#4233,#2666,.T.);
#7783=ORIENTED_EDGE('',*,*,#5405,.T.);
#7784=ORIENTED_EDGE('',*,*,#5406,.T.);
#7785=ORIENTED_EDGE('',*,*,#5407,.F.);
#7786=ORIENTED_EDGE('',*,*,#5408,.T.);
#7787=ORIENTED_EDGE('',*,*,#5409,.T.);
#7788=ORIENTED_EDGE('',*,*,#5410,.T.);
#7789=ORIENTED_EDGE('',*,*,#5405,.F.);
#7790=ORIENTED_EDGE('',*,*,#5411,.T.);
#7791=ORIENTED_EDGE('',*,*,#5412,.T.);
#7792=ORIENTED_EDGE('',*,*,#5413,.T.);
#7793=ORIENTED_EDGE('',*,*,#5409,.F.);
#7794=ORIENTED_EDGE('',*,*,#5414,.T.);
#7795=ORIENTED_EDGE('',*,*,#5415,.F.);
#7796=ORIENTED_EDGE('',*,*,#5416,.T.);
#7797=ORIENTED_EDGE('',*,*,#5417,.F.);
#7798=ORIENTED_EDGE('',*,*,#5418,.T.);
#7799=ORIENTED_EDGE('',*,*,#5419,.T.);
#7800=ORIENTED_EDGE('',*,*,#5420,.T.);
#7801=ORIENTED_EDGE('',*,*,#5421,.F.);
#7802=ORIENTED_EDGE('',*,*,#5422,.F.);
#7803=ORIENTED_EDGE('',*,*,#5423,.T.);
#7804=ORIENTED_EDGE('',*,*,#5424,.T.);
#7805=ORIENTED_EDGE('',*,*,#5419,.F.);
#7806=ORIENTED_EDGE('',*,*,#5425,.F.);
#7807=ORIENTED_EDGE('',*,*,#5426,.T.);
#7808=ORIENTED_EDGE('',*,*,#5427,.T.);
#7809=ORIENTED_EDGE('',*,*,#5423,.F.);
#7810=ORIENTED_EDGE('',*,*,#5428,.F.);
#7811=ORIENTED_EDGE('',*,*,#5429,.F.);
#7812=ORIENTED_EDGE('',*,*,#5430,.F.);
#7813=ORIENTED_EDGE('',*,*,#5431,.F.);
#7814=ORIENTED_EDGE('',*,*,#5432,.T.);
#7815=ORIENTED_EDGE('',*,*,#5429,.T.);
#7816=ORIENTED_EDGE('',*,*,#5433,.T.);
#7817=ORIENTED_EDGE('',*,*,#5426,.F.);
#7818=ORIENTED_EDGE('',*,*,#5434,.F.);
#7819=ORIENTED_EDGE('',*,*,#5435,.F.);
#7820=ORIENTED_EDGE('',*,*,#5420,.F.);
#7821=ORIENTED_EDGE('',*,*,#5424,.F.);
#7822=ORIENTED_EDGE('',*,*,#5427,.F.);
#7823=ORIENTED_EDGE('',*,*,#5433,.F.);
#7824=ORIENTED_EDGE('',*,*,#5432,.F.);
#7825=ORIENTED_EDGE('',*,*,#5436,.F.);
#7826=ORIENTED_EDGE('',*,*,#5416,.F.);
#7827=ORIENTED_EDGE('',*,*,#5437,.F.);
#7828=ORIENTED_EDGE('',*,*,#5414,.F.);
#7829=ORIENTED_EDGE('',*,*,#5411,.F.);
#7830=ORIENTED_EDGE('',*,*,#5408,.F.);
#7831=ORIENTED_EDGE('',*,*,#5438,.F.);
#7832=ORIENTED_EDGE('',*,*,#5406,.F.);
#7833=ORIENTED_EDGE('',*,*,#5410,.F.);
#7834=ORIENTED_EDGE('',*,*,#5413,.F.);
#7835=ORIENTED_EDGE('',*,*,#5439,.F.);
#7836=ORIENTED_EDGE('',*,*,#5418,.F.);
#7837=ORIENTED_EDGE('',*,*,#5440,.F.);
#7838=ORIENTED_EDGE('',*,*,#5430,.T.);
#7839=ORIENTED_EDGE('',*,*,#5434,.T.);
#7840=ORIENTED_EDGE('',*,*,#5428,.T.);
#7841=ORIENTED_EDGE('',*,*,#5425,.T.);
#7842=ORIENTED_EDGE('',*,*,#5422,.T.);
#7843=ORIENTED_EDGE('',*,*,#5441,.T.);
#7844=ORIENTED_EDGE('',*,*,#5442,.T.);
#7845=ORIENTED_EDGE('',*,*,#5443,.T.);
#7846=ORIENTED_EDGE('',*,*,#5444,.T.);
#7847=ORIENTED_EDGE('',*,*,#5445,.T.);
#7848=ORIENTED_EDGE('',*,*,#5446,.T.);
#7849=ORIENTED_EDGE('',*,*,#5438,.T.);
#7850=ORIENTED_EDGE('',*,*,#5421,.T.);
#7851=ORIENTED_EDGE('',*,*,#5435,.T.);
#7852=ORIENTED_EDGE('',*,*,#5407,.T.);
#7853=ORIENTED_EDGE('',*,*,#5415,.T.);
#7854=ORIENTED_EDGE('',*,*,#5439,.T.);
#7855=ORIENTED_EDGE('',*,*,#5412,.F.);
#7856=ORIENTED_EDGE('',*,*,#5437,.T.);
#7857=ORIENTED_EDGE('',*,*,#5447,.T.);
#7858=ORIENTED_EDGE('',*,*,#5448,.T.);
#7859=ORIENTED_EDGE('',*,*,#5446,.F.);
#7860=ORIENTED_EDGE('',*,*,#5449,.F.);
#7861=ORIENTED_EDGE('',*,*,#5450,.T.);
#7862=ORIENTED_EDGE('',*,*,#5449,.T.);
#7863=ORIENTED_EDGE('',*,*,#5445,.F.);
#7864=ORIENTED_EDGE('',*,*,#5451,.F.);
#7865=ORIENTED_EDGE('',*,*,#5452,.T.);
#7866=ORIENTED_EDGE('',*,*,#5451,.T.);
#7867=ORIENTED_EDGE('',*,*,#5444,.F.);
#7868=ORIENTED_EDGE('',*,*,#5453,.F.);
#7869=ORIENTED_EDGE('',*,*,#5454,.T.);
#7870=ORIENTED_EDGE('',*,*,#5453,.T.);
#7871=ORIENTED_EDGE('',*,*,#5443,.F.);
#7872=ORIENTED_EDGE('',*,*,#5455,.F.);
#7873=ORIENTED_EDGE('',*,*,#5456,.T.);
#7874=ORIENTED_EDGE('',*,*,#5455,.T.);
#7875=ORIENTED_EDGE('',*,*,#5442,.F.);
#7876=ORIENTED_EDGE('',*,*,#5457,.F.);
#7877=ORIENTED_EDGE('',*,*,#5458,.T.);
#7878=ORIENTED_EDGE('',*,*,#5457,.T.);
#7879=ORIENTED_EDGE('',*,*,#5441,.F.);
#7880=ORIENTED_EDGE('',*,*,#5448,.F.);
#7881=ORIENTED_EDGE('',*,*,#5458,.F.);
#7882=ORIENTED_EDGE('',*,*,#5447,.F.);
#7883=ORIENTED_EDGE('',*,*,#5450,.F.);
#7884=ORIENTED_EDGE('',*,*,#5452,.F.);
#7885=ORIENTED_EDGE('',*,*,#5454,.F.);
#7886=ORIENTED_EDGE('',*,*,#5456,.F.);
#7887=ORIENTED_EDGE('',*,*,#5440,.T.);
#7888=ORIENTED_EDGE('',*,*,#5417,.T.);
#7889=ORIENTED_EDGE('',*,*,#5436,.T.);
#7890=ORIENTED_EDGE('',*,*,#5431,.T.);
#8261=CYLINDRICAL_SURFACE('',#9672,1.0501);
#8262=CYLINDRICAL_SURFACE('',#9674,1.0501);
#8263=CYLINDRICAL_SURFACE('',#9675,1.0501);
#8264=CYLINDRICAL_SURFACE('',#9676,1.0501);
#8265=CYLINDRICAL_SURFACE('',#9678,1.21745);
#8266=CYLINDRICAL_SURFACE('',#9680,1.21745);
#8267=CYLINDRICAL_SURFACE('',#9681,1.21745);
#8268=CYLINDRICAL_SURFACE('',#9682,1.21745);
#8269=CYLINDRICAL_SURFACE('',#9684,1.21745);
#8270=CYLINDRICAL_SURFACE('',#9686,1.0501);
#8728=ADVANCED_FACE('',(#1491),#8261,.F.);
#8729=ADVANCED_FACE('',(#1492),#8262,.F.);
#8730=ADVANCED_FACE('',(#1493),#8263,.F.);
#8731=ADVANCED_FACE('',(#1494),#8264,.F.);
#8732=ADVANCED_FACE('',(#1495),#8265,.F.);
#8733=ADVANCED_FACE('',(#1496),#8266,.F.);
#8734=ADVANCED_FACE('',(#1497),#8267,.F.);
#8735=ADVANCED_FACE('',(#1498),#8268,.F.);
#8736=ADVANCED_FACE('',(#1499),#8269,.F.);
#8737=ADVANCED_FACE('',(#1500),#213,.F.);
#8738=ADVANCED_FACE('',(#1501),#214,.F.);
#8739=ADVANCED_FACE('',(#1502,#853),#1028,.T.);
#8740=ADVANCED_FACE('',(#1503),#8270,.F.);
#8741=ADVANCED_FACE('',(#1504),#1029,.T.);
#8742=ADVANCED_FACE('',(#1505),#1030,.T.);
#8743=ADVANCED_FACE('',(#1506),#1031,.T.);
#8744=ADVANCED_FACE('',(#1507),#1032,.T.);
#8745=ADVANCED_FACE('',(#1508),#1033,.T.);
#8746=ADVANCED_FACE('',(#1509),#1034,.T.);
#8747=ADVANCED_FACE('',(#1510,#854),#1035,.F.);
#8798=CLOSED_SHELL('',(#8728,#8729,#8730,#8731,#8732,#8733,#8734,#8735,
#8736,#8737,#8738,#8739,#8740,#8741,#8742,#8743,#8744,#8745,#8746,#8747));
#9671=AXIS2_PLACEMENT_3D('',#31658,#11546,#11547);
#9672=AXIS2_PLACEMENT_3D('',#31659,#11548,#11549);
#9673=AXIS2_PLACEMENT_3D('',#31672,#11551,#11552);
#9674=AXIS2_PLACEMENT_3D('',#31692,#11553,#11554);
#9675=AXIS2_PLACEMENT_3D('',#31782,#11556,#11557);
#9676=AXIS2_PLACEMENT_3D('',#31872,#11559,#11560);
#9677=AXIS2_PLACEMENT_3D('',#31903,#11562,#11563);
#9678=AXIS2_PLACEMENT_3D('',#31941,#11564,#11565);
#9679=AXIS2_PLACEMENT_3D('',#31960,#11567,#11568);
#9680=AXIS2_PLACEMENT_3D('',#31975,#11569,#11570);
#9681=AXIS2_PLACEMENT_3D('',#32013,#11572,#11573);
#9682=AXIS2_PLACEMENT_3D('',#32051,#11575,#11576);
#9683=AXIS2_PLACEMENT_3D('',#32063,#11578,#11579);
#9684=AXIS2_PLACEMENT_3D('',#32071,#11580,#11581);
#9685=AXIS2_PLACEMENT_3D('',#32974,#11582,#11583);
#9686=AXIS2_PLACEMENT_3D('',#32987,#11590,#11591);
#9687=AXIS2_PLACEMENT_3D('',#32988,#11592,#11593);
#9688=AXIS2_PLACEMENT_3D('',#32994,#11597,#11598);
#9689=AXIS2_PLACEMENT_3D('',#32998,#11601,#11602);
#9690=AXIS2_PLACEMENT_3D('',#33002,#11605,#11606);
#9691=AXIS2_PLACEMENT_3D('',#33006,#11609,#11610);
#9692=AXIS2_PLACEMENT_3D('',#33010,#11613,#11614);
#9693=AXIS2_PLACEMENT_3D('',#33012,#11616,#11617);
#11546=DIRECTION('axis',(0.,0.,1.));
#11547=DIRECTION('refdir',(1.,0.,0.));
#11548=DIRECTION('center_axis',(0.,0.,1.));
#11549=DIRECTION('ref_axis',(-0.349612887919324,-0.936894246220303,0.));
#11550=DIRECTION('',(0.,0.,1.));
#11551=DIRECTION('center_axis',(0.,0.,-1.));
#11552=DIRECTION('ref_axis',(1.,0.,0.));
#11553=DIRECTION('center_axis',(0.,0.,1.));
#11554=DIRECTION('ref_axis',(1.,0.,0.));
#11555=DIRECTION('',(0.,0.,1.));
#11556=DIRECTION('center_axis',(0.,0.,1.));
#11557=DIRECTION('ref_axis',(1.,0.,0.));
#11558=DIRECTION('',(0.,0.,1.));
#11559=DIRECTION('center_axis',(0.,0.,1.));
#11560=DIRECTION('ref_axis',(0.936891240421608,0.349620942766964,0.));
#11561=DIRECTION('',(0.,0.,1.));
#11562=DIRECTION('center_axis',(0.,0.,-1.));
#11563=DIRECTION('ref_axis',(1.,0.,0.));
#11564=DIRECTION('center_axis',(0.,0.,1.));
#11565=DIRECTION('ref_axis',(1.,3.79078190120237E-16,0.));
#11566=DIRECTION('',(1.22464679914735E-16,6.14212870423506E-32,1.));
#11567=DIRECTION('center_axis',(0.,0.,-1.));
#11568=DIRECTION('ref_axis',(1.,3.79078190120237E-16,0.));
#11569=DIRECTION('center_axis',(0.,0.,1.));
#11570=DIRECTION('ref_axis',(1.,3.79078190120237E-16,0.));
#11571=DIRECTION('',(1.22464679914735E-16,6.14212870423506E-32,1.));
#11572=DIRECTION('center_axis',(0.,0.,1.));
#11573=DIRECTION('ref_axis',(1.,3.79078190120237E-16,0.));
#11574=DIRECTION('',(1.22464679914735E-16,6.14212870423506E-32,1.));
#11575=DIRECTION('center_axis',(0.,0.,1.));
#11576=DIRECTION('ref_axis',(-0.608868431756822,0.793271222729016,0.));
#11577=DIRECTION('',(1.22464679914735E-16,6.14212870423506E-32,1.));
#11578=DIRECTION('center_axis',(0.,0.,1.));
#11579=DIRECTION('ref_axis',(1.,3.79078190120237E-16,0.));
#11580=DIRECTION('center_axis',(0.,0.,1.));
#11581=DIRECTION('ref_axis',(1.,3.79078190120237E-16,0.));
#11582=DIRECTION('center_axis',(0.,0.,1.));
#11583=DIRECTION('ref_axis',(1.,0.,0.));
#11584=DIRECTION('',(0.5,0.866025403784439,0.));
#11585=DIRECTION('',(-0.5,0.866025403784439,0.));
#11586=DIRECTION('',(-1.,0.,0.));
#11587=DIRECTION('',(-0.5,-0.866025403784439,0.));
#11588=DIRECTION('',(0.499999999999999,-0.866025403784439,0.));
#11589=DIRECTION('',(1.,-2.13662520709285E-16,0.));
#11590=DIRECTION('center_axis',(0.,0.,1.));
#11591=DIRECTION('ref_axis',(1.,0.,0.));
#11592=DIRECTION('center_axis',(-2.13662520709285E-16,-1.,0.));
#11593=DIRECTION('ref_axis',(1.,-2.13662520709285E-16,0.));
#11594=DIRECTION('',(1.,-2.13662520709285E-16,0.));
#11595=DIRECTION('',(0.,0.,1.));
#11596=DIRECTION('',(0.,0.,1.));
#11597=DIRECTION('center_axis',(-0.866025403784439,-0.499999999999999,0.));
#11598=DIRECTION('ref_axis',(0.499999999999999,-0.866025403784439,0.));
#11599=DIRECTION('',(0.499999999999999,-0.866025403784439,0.));
#11600=DIRECTION('',(0.,0.,1.));
#11601=DIRECTION('center_axis',(-0.866025403784439,0.5,0.));
#11602=DIRECTION('ref_axis',(-0.5,-0.866025403784439,0.));
#11603=DIRECTION('',(-0.5,-0.866025403784439,0.));
#11604=DIRECTION('',(0.,0.,1.));
#11605=DIRECTION('center_axis',(0.,1.,0.));
#11606=DIRECTION('ref_axis',(-1.,0.,0.));
#11607=DIRECTION('',(-1.,0.,0.));
#11608=DIRECTION('',(0.,0.,1.));
#11609=DIRECTION('center_axis',(0.866025403784439,0.5,0.));
#11610=DIRECTION('ref_axis',(-0.5,0.866025403784439,0.));
#11611=DIRECTION('',(-0.5,0.866025403784439,0.));
#11612=DIRECTION('',(0.,0.,1.));
#11613=DIRECTION('center_axis',(0.866025403784439,-0.5,0.));
#11614=DIRECTION('ref_axis',(0.5,0.866025403784439,0.));
#11615=DIRECTION('',(0.5,0.866025403784439,0.));
#11616=DIRECTION('center_axis',(0.,0.,1.));
#11617=DIRECTION('ref_axis',(1.,0.,0.));
#31658=CARTESIAN_POINT('',(0.,0.,0.));
#31659=CARTESIAN_POINT('Origin',(-8.5,0.,22.7));
#31660=CARTESIAN_POINT('',(-9.55012850889018,-2.18470748328814E-5,23.8841069671524));
#31661=CARTESIAN_POINT('',(-9.55000870253874,1.05562245468413E-6,23.9658930328476));
#31662=CARTESIAN_POINT('',(-9.5501,-1.28600160378464E-16,22.7));
#31663=CARTESIAN_POINT('',(-9.29338130674011,-0.687936125025682,24.));
#31664=CARTESIAN_POINT('Ctrl Pts',(-9.55000870253874,1.05562245468413E-6,
23.9658930328476));
#31665=CARTESIAN_POINT('Ctrl Pts',(-9.55001614030791,-0.0803132194169134,
23.9695440482821));
#31666=CARTESIAN_POINT('Ctrl Pts',(-9.54090449002282,-0.160622529114386,
23.9731950637165));
#31667=CARTESIAN_POINT('Ctrl Pts',(-9.52264652698618,-0.238789064503808,
23.9768460791509));
#31668=CARTESIAN_POINT('Ctrl Pts',(-9.48405055840263,-0.404027275257131,
23.9845640527673));
#31669=CARTESIAN_POINT('Ctrl Pts',(-9.4045826463392,-0.559690113640418,
23.9922820263836));
#31670=CARTESIAN_POINT('Ctrl Pts',(-9.29338130674012,-0.687936125025676,
24.));
#31671=CARTESIAN_POINT('',(-7.70658052800239,-0.687941579884198,24.));
#31672=CARTESIAN_POINT('Origin',(-8.5,0.,24.));
#31673=CARTESIAN_POINT('Ctrl Pts',(-7.70658052800239,-0.687941579884198,
24.));
#31674=CARTESIAN_POINT('Ctrl Pts',(-7.79864121713694,-0.793916118632762,
23.9936166544345));
#31675=CARTESIAN_POINT('Ctrl Pts',(-7.91206802406805,-0.881431367900445,
23.987233308869));
#31676=CARTESIAN_POINT('Ctrl Pts',(-8.03812197772265,-0.94316120005307,
23.9808499633034));
#31677=CARTESIAN_POINT('Ctrl Pts',(-8.19053125567241,-1.01779748771859,
23.9731319896871));
#31678=CARTESIAN_POINT('Ctrl Pts',(-8.36139982794667,-1.05473875098712,
23.9654140160707));
#31679=CARTESIAN_POINT('Ctrl Pts',(-8.53102865307542,-1.04972479101945,
23.9576960424544));
#31680=CARTESIAN_POINT('Ctrl Pts',(-8.70065747820416,-1.04471083105178,
23.949978068838));
#31681=CARTESIAN_POINT('Ctrl Pts',(-8.86904655618739,-0.997741647847902,
23.9422600952216));
#31682=CARTESIAN_POINT('Ctrl Pts',(-9.01678099765897,-0.914232989059095,
23.9345421216053));
#31683=CARTESIAN_POINT('Ctrl Pts',(-9.16451543913055,-0.830724330270285,
23.9268241479889));
#31684=CARTESIAN_POINT('Ctrl Pts',(-9.29159524409048,-0.710676195896543,
23.9191061743725));
#31685=CARTESIAN_POINT('Ctrl Pts',(-9.38336905036905,-0.567929262511223,
23.9113882007562));
#31686=CARTESIAN_POINT('Ctrl Pts',(-9.47514285664761,-0.425182329125902,
23.9036702271398));
#31687=CARTESIAN_POINT('Ctrl Pts',(-9.53161066424481,-0.259736596729006,
23.8959522535235));
#31688=CARTESIAN_POINT('Ctrl Pts',(-9.54626192835179,-0.090667154812442,
23.8882342799071));
#31689=CARTESIAN_POINT('Ctrl Pts',(-9.54887359613867,-0.0605296040881374,
23.8868585089889));
#31690=CARTESIAN_POINT('Ctrl Pts',(-9.5501565429157,-0.0302769099643429,
23.8854827380706));
#31691=CARTESIAN_POINT('Ctrl Pts',(-9.55012850889018,-2.18470748328814E-5,
23.8841069671524));
#31692=CARTESIAN_POINT('Origin',(-8.5,0.,22.7));
#31693=CARTESIAN_POINT('',(-9.55014846165012,-1.85392301343956E-5,23.5841069671524));
#31694=CARTESIAN_POINT('',(-9.55002911984723,-9.63121900339139E-6,23.6658930328476));
#31695=CARTESIAN_POINT('',(-9.5501,-1.28600160378464E-16,22.7));
#31696=CARTESIAN_POINT('Ctrl Pts',(-9.55002911984723,-9.63121900339139E-6,
23.6658930328476));
#31697=CARTESIAN_POINT('Ctrl Pts',(-9.55005395760937,-0.0729827112292251,
23.6692103912693));
#31698=CARTESIAN_POINT('Ctrl Pts',(-9.54254664910082,-0.14595075200247,
23.6725277496911));
#31699=CARTESIAN_POINT('Ctrl Pts',(-9.52745273693827,-0.21731416785282,
23.6758451081128));
#31700=CARTESIAN_POINT('Ctrl Pts',(-9.49233611671553,-0.383344150353556,
23.6835630817291));
#31701=CARTESIAN_POINT('Ctrl Pts',(-9.41615474671242,-0.540688622979868,
23.6912810553455));
#31702=CARTESIAN_POINT('Ctrl Pts',(-9.30769192489819,-0.671206621789361,
23.6989990289619));
#31703=CARTESIAN_POINT('Ctrl Pts',(-9.19922910308395,-0.801724620598853,
23.7067170025782));
#31704=CARTESIAN_POINT('Ctrl Pts',(-9.0584848294586,-0.905416145591528,
23.7144349761946));
#31705=CARTESIAN_POINT('Ctrl Pts',(-8.90168615075291,-0.970326134859246,
23.722152949811));
#31706=CARTESIAN_POINT('Ctrl Pts',(-8.74488747204723,-1.03523612412696,
23.7298709234273));
#31707=CARTESIAN_POINT('Ctrl Pts',(-8.57203438826122,-1.06136457766973,
23.7375888970437));
#31708=CARTESIAN_POINT('Ctrl Pts',(-8.40305592256279,-1.04569901309732,
23.74530687066));
#31709=CARTESIAN_POINT('Ctrl Pts',(-8.23407745686436,-1.03003344852491,
23.7530248442764));
#31710=CARTESIAN_POINT('Ctrl Pts',(-8.06897360925351,-0.972573865837326,
23.7607428178928));
#31711=CARTESIAN_POINT('Ctrl Pts',(-7.926779946155,-0.879945072400683,23.7684607915091));
#31712=CARTESIAN_POINT('Ctrl Pts',(-7.7845862830565,-0.78731627896404,23.7761787651255));
#31713=CARTESIAN_POINT('Ctrl Pts',(-7.66530280447034,-0.659518274778334,
23.7838967387419));
#31714=CARTESIAN_POINT('Ctrl Pts',(-7.5826822635998,-0.511285407188883,
23.7916147123582));
#31715=CARTESIAN_POINT('Ctrl Pts',(-7.50006172272926,-0.363052539599431,
23.7993326859746));
#31716=CARTESIAN_POINT('Ctrl Pts',(-7.45410411957434,-0.194384808606232,
23.8070506595909));
#31717=CARTESIAN_POINT('Ctrl Pts',(-7.45010807549069,-0.0247288294128955,
23.8147686332073));
#31718=CARTESIAN_POINT('Ctrl Pts',(-7.44611203140704,0.144927149780442,
23.8224866068237));
#31719=CARTESIAN_POINT('Ctrl Pts',(-7.48407754639465,0.315571377173915,
23.83020458044));
#31720=CARTESIAN_POINT('Ctrl Pts',(-7.55962748533197,0.467529822444092,
23.8379225540564));
#31721=CARTESIAN_POINT('Ctrl Pts',(-7.63517742426929,0.619488267714268,
23.8456405276727));
#31722=CARTESIAN_POINT('Ctrl Pts',(-7.7483117871563,0.752760930861145,23.8533585012891));
#31723=CARTESIAN_POINT('Ctrl Pts',(-7.88598660108357,0.851981517213941,
23.8610764749055));
#31724=CARTESIAN_POINT('Ctrl Pts',(-8.02366141501085,0.951202103566738,
23.8687944485218));
#31725=CARTESIAN_POINT('Ctrl Pts',(-8.18587667997837,1.01637061312545,23.8765124221382));
#31726=CARTESIAN_POINT('Ctrl Pts',(-8.35393023216907,1.03997501555327,23.8842303957546));
#31727=CARTESIAN_POINT('Ctrl Pts',(-8.52198378435977,1.06357941798109,23.8919483693709));
#31728=CARTESIAN_POINT('Ctrl Pts',(-8.69587562377364,1.04561971327801,23.8996663429873));
#31729=CARTESIAN_POINT('Ctrl Pts',(-8.85555596986305,0.988163359218205,
23.9073843166037));
#31730=CARTESIAN_POINT('Ctrl Pts',(-9.01523631595246,0.930707005158396,
23.91510229022));
#31731=CARTESIAN_POINT('Ctrl Pts',(-9.1607051687174,0.833754001741858,23.9228202638364));
#31732=CARTESIAN_POINT('Ctrl Pts',(-9.27519234914899,0.708490052395413,
23.9305382374527));
#31733=CARTESIAN_POINT('Ctrl Pts',(-9.38967952958059,0.583226103048967,
23.9382562110691));
#31734=CARTESIAN_POINT('Ctrl Pts',(-9.47318503767883,0.429651207772614,
23.9459741846855));
#31735=CARTESIAN_POINT('Ctrl Pts',(-9.51607577917611,0.265456968572753,
23.9536921583018));
#31736=CARTESIAN_POINT('Ctrl Pts',(-9.53867689972046,0.178935410229467,
23.9577591164838));
#31737=CARTESIAN_POINT('Ctrl Pts',(-9.55000041742005,0.0894651523548535,
23.9618260746657));
#31738=CARTESIAN_POINT('Ctrl Pts',(-9.55000870253874,1.05562245468413E-6,
23.9658930328476));
#31739=CARTESIAN_POINT('Ctrl Pts',(-9.55012850889018,-2.18470748328814E-5,
23.8841069671524));
#31740=CARTESIAN_POINT('Ctrl Pts',(-9.54999927409541,0.139451766551989,
23.8777647644543));
#31741=CARTESIAN_POINT('Ctrl Pts',(-9.52200983360965,0.278975719817604,
23.8714225617561));
#31742=CARTESIAN_POINT('Ctrl Pts',(-9.46789815100873,0.407501764958256,
23.865080359058));
#31743=CARTESIAN_POINT('Ctrl Pts',(-9.40204838894191,0.563908091376159,
23.8573623854417));
#31744=CARTESIAN_POINT('Ctrl Pts',(-9.2975141441915,0.704027592775735,23.8496444118253));
#31745=CARTESIAN_POINT('Ctrl Pts',(-9.1663476221531,0.811705232975747,23.8419264382089));
#31746=CARTESIAN_POINT('Ctrl Pts',(-9.03518110011469,0.919382873175757,
23.8342084645926));
#31747=CARTESIAN_POINT('Ctrl Pts',(-8.8773823007883,0.994618652176204,23.8264904909762));
#31748=CARTESIAN_POINT('Ctrl Pts',(-8.71114457750307,1.02873830379683,23.8187725173598));
#31749=CARTESIAN_POINT('Ctrl Pts',(-8.54490685421784,1.06285795541745,23.8110545437435));
#31750=CARTESIAN_POINT('Ctrl Pts',(-8.37023020697377,1.05586147965824,23.8033365701271));
#31751=CARTESIAN_POINT('Ctrl Pts',(-8.20725389715392,1.00855552775547,23.7956185965107));
#31752=CARTESIAN_POINT('Ctrl Pts',(-8.04427758733408,0.961249575852697,
23.7879006228944));
#31753=CARTESIAN_POINT('Ctrl Pts',(-7.89300161493846,0.873634147806356,
23.780182649278));
#31754=CARTESIAN_POINT('Ctrl Pts',(-7.77086727824076,0.755810827431719,
23.7724646756617));
#31755=CARTESIAN_POINT('Ctrl Pts',(-7.64873294154307,0.63798750705708,23.7647467020453));
#31756=CARTESIAN_POINT('Ctrl Pts',(-7.5557402405433,0.489956294354147,23.7570287284289));
#31757=CARTESIAN_POINT('Ctrl Pts',(-7.50261072631204,0.328784381272252,
23.7493107548126));
#31758=CARTESIAN_POINT('Ctrl Pts',(-7.44948121208079,0.167612468190361,
23.7415927811962));
#31759=CARTESIAN_POINT('Ctrl Pts',(-7.43621488461805,-0.00670014527048846,
23.7338748075799));
#31760=CARTESIAN_POINT('Ctrl Pts',(-7.464341279731,-0.174056163419163,23.7261568339635));
#31761=CARTESIAN_POINT('Ctrl Pts',(-7.49246767484396,-0.34141218156784,
23.7184388603471));
#31762=CARTESIAN_POINT('Ctrl Pts',(-7.5619867925326,-0.501811604404344,
23.7107208867308));
#31763=CARTESIAN_POINT('Ctrl Pts',(-7.66488345680942,-0.63676125197269,
23.7030029131144));
#31764=CARTESIAN_POINT('Ctrl Pts',(-7.76778012108624,-0.771710899541037,
23.695284939498));
#31765=CARTESIAN_POINT('Ctrl Pts',(-7.90405433195122,-0.881210771841228,
23.6875669658817));
#31766=CARTESIAN_POINT('Ctrl Pts',(-8.05799441494728,-0.952636129689753,
23.6798489922653));
#31767=CARTESIAN_POINT('Ctrl Pts',(-8.21193449794334,-1.02406148753828,
23.672131018649));
#31768=CARTESIAN_POINT('Ctrl Pts',(-8.38354045307049,-1.05741233093514,
23.6644130450326));
#31769=CARTESIAN_POINT('Ctrl Pts',(-8.55302704797763,-1.04884348925778,
23.6566950714162));
#31770=CARTESIAN_POINT('Ctrl Pts',(-8.72251364288478,-1.04027464758041,
23.6489770977999));
#31771=CARTESIAN_POINT('Ctrl Pts',(-8.88988087757193,-0.989786120828835,
23.6412591241835));
#31772=CARTESIAN_POINT('Ctrl Pts',(-9.03583222114397,-0.903198961230685,
23.6335411505671));
#31773=CARTESIAN_POINT('Ctrl Pts',(-9.18178356471601,-0.816611801632534,
23.6258231769508));
#31774=CARTESIAN_POINT('Ctrl Pts',(-9.30631901717293,-0.693926009187812,
23.6181052033344));
#31775=CARTESIAN_POINT('Ctrl Pts',(-9.39508031887919,-0.549286587801987,
23.6103872297181));
#31776=CARTESIAN_POINT('Ctrl Pts',(-9.48384162058545,-0.404647166416162,
23.6026692561017));
#31777=CARTESIAN_POINT('Ctrl Pts',(-9.53682877154105,-0.238054116089234,
23.5949512824853));
#31778=CARTESIAN_POINT('Ctrl Pts',(-9.54793264173766,-0.0687147084919738,
23.587233308869));
#31779=CARTESIAN_POINT('Ctrl Pts',(-9.54943193392396,-0.0458497752616798,
23.5861911949634));
#31780=CARTESIAN_POINT('Ctrl Pts',(-9.55016762861391,-0.0229347716572958,
23.5851490810579));
#31781=CARTESIAN_POINT('Ctrl Pts',(-9.55014846165012,-1.85392301343956E-5,
23.5841069671524));
#31782=CARTESIAN_POINT('Origin',(-8.5,0.,22.7));
#31783=CARTESIAN_POINT('',(-9.55016549375182,-1.36966017015294E-5,23.2841069671524));
#31784=CARTESIAN_POINT('',(-9.55003901931283,-1.48519368357603E-5,23.3658930328476));
#31785=CARTESIAN_POINT('',(-9.5501,-1.28600160378464E-16,22.7));
#31786=CARTESIAN_POINT('Ctrl Pts',(-9.55003901931283,-1.48519368357603E-5,
23.3658930328476));
#31787=CARTESIAN_POINT('Ctrl Pts',(-9.55007393234815,-0.0656465877237161,
23.3688767342566));
#31788=CARTESIAN_POINT('Ctrl Pts',(-9.54400975139509,-0.131271950178925,
23.3718604356656));
#31789=CARTESIAN_POINT('Ctrl Pts',(-9.53178246487035,-0.195728177219803,
23.3748441370746));
#31790=CARTESIAN_POINT('Ctrl Pts',(-9.50015400683739,-0.36245781652283,
23.382562110691));
#31791=CARTESIAN_POINT('Ctrl Pts',(-9.42728775074502,-0.521364683757543,
23.3902800843074));
#31792=CARTESIAN_POINT('Ctrl Pts',(-9.32158477919497,-0.654127682311983,
23.3979980579237));
#31793=CARTESIAN_POINT('Ctrl Pts',(-9.21588180764493,-0.786890680866422,
23.4057160315401));
#31794=CARTESIAN_POINT('Ctrl Pts',(-9.07734212063722,-0.893509810740587,
23.4134340051565));
#31795=CARTESIAN_POINT('Ctrl Pts',(-8.92193858979441,-0.961692466755417,
23.4211519787728));
#31796=CARTESIAN_POINT('Ctrl Pts',(-8.76653505895159,-1.02987512277025,
23.4288699523892));
#31797=CARTESIAN_POINT('Ctrl Pts',(-8.59426768427367,-1.05962130492574,
23.4365879260056));
#31798=CARTESIAN_POINT('Ctrl Pts',(-8.42499795613852,-1.04750144037518,
23.4443058996219));
#31799=CARTESIAN_POINT('Ctrl Pts',(-8.25572822800336,-1.03538157582462,
23.4520238732383));
#31800=CARTESIAN_POINT('Ctrl Pts',(-8.08945614641095,-0.981395664568007,
23.4597418468546));
#31801=CARTESIAN_POINT('Ctrl Pts',(-7.94535197708869,-0.891767988241791,
23.467459820471));
#31802=CARTESIAN_POINT('Ctrl Pts',(-7.80124780776642,-0.802140311915576,
23.4751777940874));
#31803=CARTESIAN_POINT('Ctrl Pts',(-7.67931155071428,-0.676870870519757,
23.4828957677037));
#31804=CARTESIAN_POINT('Ctrl Pts',(-7.59360179247881,-0.530402548611195,
23.4906137413201));
#31805=CARTESIAN_POINT('Ctrl Pts',(-7.50789203424333,-0.383934226702632,
23.4983317149364));
#31806=CARTESIAN_POINT('Ctrl Pts',(-7.45840877482451,-0.216267024281328,
23.5060496885528));
#31807=CARTESIAN_POINT('Ctrl Pts',(-7.45085716461962,-0.0467320569044314,
23.5137676621692));
#31808=CARTESIAN_POINT('Ctrl Pts',(-7.44330555441472,0.122802910472465,
23.5214856357855));
#31809=CARTESIAN_POINT('Ctrl Pts',(-7.47768559342375,0.294205642804954,
23.5292036094019));
#31810=CARTESIAN_POINT('Ctrl Pts',(-7.5500334503303,0.44771433825753,23.5369215830183));
#31811=CARTESIAN_POINT('Ctrl Pts',(-7.62238130723685,0.601223033710108,
23.5446395566346));
#31812=CARTESIAN_POINT('Ctrl Pts',(-7.73269698204091,0.736837692282775,
23.552357530251));
#31813=CARTESIAN_POINT('Ctrl Pts',(-7.8682616780666,0.838922682232956,23.5600755038673));
#31814=CARTESIAN_POINT('Ctrl Pts',(-8.00382637409228,0.941007672183136,
23.5677934774837));
#31815=CARTESIAN_POINT('Ctrl Pts',(-8.1646400913396,1.00956299351083,23.5755114511001));
#31816=CARTESIAN_POINT('Ctrl Pts',(-8.33216188375618,1.0366845908627,23.5832294247164));
#31817=CARTESIAN_POINT('Ctrl Pts',(-8.49968367617277,1.06380618821457,23.5909473983328));
#31818=CARTESIAN_POINT('Ctrl Pts',(-8.67391354375863,1.04949406159062,23.5986653719492));
#31819=CARTESIAN_POINT('Ctrl Pts',(-8.83476373142291,0.995398321395473,
23.6063833455655));
#31820=CARTESIAN_POINT('Ctrl Pts',(-8.99561391908718,0.94130258120033,23.6141013191819));
#31821=CARTESIAN_POINT('Ctrl Pts',(-9.14308442682988,0.847423227433994,
23.6218192927983));
#31822=CARTESIAN_POINT('Ctrl Pts',(-9.26017270794676,0.724584038172587,
23.6295372664146));
#31823=CARTESIAN_POINT('Ctrl Pts',(-9.37726098906364,0.601744848911179,
23.637255240031));
#31824=CARTESIAN_POINT('Ctrl Pts',(-9.4639670435547,0.449945824154699,23.6449732136473));
#31825=CARTESIAN_POINT('Ctrl Pts',(-9.51029413557904,0.286688565588882,
23.6526911872637));
#31826=CARTESIAN_POINT('Ctrl Pts',(-9.53670880285049,0.193602943845163,
23.6570918024583));
#31827=CARTESIAN_POINT('Ctrl Pts',(-9.54999617151317,0.0967922225061255,
23.661492417653));
#31828=CARTESIAN_POINT('Ctrl Pts',(-9.55002911984723,-9.63121900339139E-6,
23.6658930328476));
#31829=CARTESIAN_POINT('Ctrl Pts',(-9.55014846165012,-1.85392301343956E-5,
23.5841069671524));
#31830=CARTESIAN_POINT('Ctrl Pts',(-9.5500256766449,0.146784561633176,23.5774311074415));
#31831=CARTESIAN_POINT('Ctrl Pts',(-9.51892503357627,0.293638090674144,
23.5707552477307));
#31832=CARTESIAN_POINT('Ctrl Pts',(-9.45914310850558,0.427702034353384,
23.5640793880199));
#31833=CARTESIAN_POINT('Ctrl Pts',(-9.39002911563927,0.582693604733889,
23.5563614144035));
#31834=CARTESIAN_POINT('Ctrl Pts',(-9.28258054046903,0.720590980627308,
23.5486434407872));
#31835=CARTESIAN_POINT('Ctrl Pts',(-9.14918561870127,0.825495345386306,
23.5409254671708));
#31836=CARTESIAN_POINT('Ctrl Pts',(-9.01579069693351,0.930399710145303,
23.5332074935544));
#31837=CARTESIAN_POINT('Ctrl Pts',(-8.85644942856823,1.00231106376988,23.5254895199381));
#31838=CARTESIAN_POINT('Ctrl Pts',(-8.68953299430229,1.0329384187134,23.5177715463217));
#31839=CARTESIAN_POINT('Ctrl Pts',(-8.52261656003635,1.06356577365693,23.5100535727053));
#31840=CARTESIAN_POINT('Ctrl Pts',(-8.34812495986976,1.05290912991939,23.502335599089));
#31841=CARTESIAN_POINT('Ctrl Pts',(-8.1861761252696,1.00219714050302,23.4946176254726));
#31842=CARTESIAN_POINT('Ctrl Pts',(-8.02422729066943,0.951485151086648,
23.4868996518563));
#31843=CARTESIAN_POINT('Ctrl Pts',(-7.87482122163571,0.860717815991441,
23.4791816782399));
#31844=CARTESIAN_POINT('Ctrl Pts',(-7.75518362447561,0.740360114764396,
23.4714637046235));
#31845=CARTESIAN_POINT('Ctrl Pts',(-7.63554602731551,0.620002413537354,
23.4637457310072));
#31846=CARTESIAN_POINT('Ctrl Pts',(-7.54567690202903,0.470054346178473,
23.4560277573908));
#31847=CARTESIAN_POINT('Ctrl Pts',(-7.49593766946272,0.307804108450993,
23.4483097837744));
#31848=CARTESIAN_POINT('Ctrl Pts',(-7.44619843689641,0.145553870723511,
23.4405918101581));
#31849=CARTESIAN_POINT('Ctrl Pts',(-7.43658909705025,-0.0289985373725711,
23.4328738365417));
#31850=CARTESIAN_POINT('Ctrl Pts',(-7.46821755448973,-0.195728173547128,
23.4251558629254));
#31851=CARTESIAN_POINT('Ctrl Pts',(-7.49984601192921,-0.362457809721686,
23.417437889309));
#31852=CARTESIAN_POINT('Ctrl Pts',(-7.57271226665433,-0.521364673974718,
23.4097199156926));
#31853=CARTESIAN_POINT('Ctrl Pts',(-7.67841523622097,-0.654127670038036,
23.4020019420763));
#31854=CARTESIAN_POINT('Ctrl Pts',(-7.78411820578762,-0.786890666101354,
23.3942839684599));
#31855=CARTESIAN_POINT('Ctrl Pts',(-7.92265789019581,-0.893509793974957,
23.3865659948436));
#31856=CARTESIAN_POINT('Ctrl Pts',(-8.07806141812267,-0.961692448710438,
23.3788480212272));
#31857=CARTESIAN_POINT('Ctrl Pts',(-8.23346494604952,-1.02987510344592,
23.3711300476108));
#31858=CARTESIAN_POINT('Ctrl Pts',(-8.40573231749505,-1.05962128504328,
23.3634120739945));
#31859=CARTESIAN_POINT('Ctrl Pts',(-8.57500204245408,-1.04750142072014,
23.3556941003781));
#31860=CARTESIAN_POINT('Ctrl Pts',(-8.7442717674131,-1.03538155639701,23.3479761267617));
#31861=CARTESIAN_POINT('Ctrl Pts',(-8.91054384588563,-0.981395646153393,
23.3402581531454));
#31862=CARTESIAN_POINT('Ctrl Pts',(-9.05464801250397,-0.89176797150894,
23.332540179529));
#31863=CARTESIAN_POINT('Ctrl Pts',(-9.19875217912231,-0.802140296864486,
23.3248222059126));
#31864=CARTESIAN_POINT('Ctrl Pts',(-9.32068843388647,-0.676870857819196,
23.3171042322963));
#31865=CARTESIAN_POINT('Ctrl Pts',(-9.40639819051372,-0.530402538658936,
23.3093862586799));
#31866=CARTESIAN_POINT('Ctrl Pts',(-9.49210794714098,-0.383934219498677,
23.3016682850636));
#31867=CARTESIAN_POINT('Ctrl Pts',(-9.54159120563132,-0.216267020223448,
23.2939503114472));
#31868=CARTESIAN_POINT('Ctrl Pts',(-9.54914281569454,-0.0467320560276536,
23.2862323378308));
#31869=CARTESIAN_POINT('Ctrl Pts',(-9.54983600155745,-0.0311699123966164,
23.285523880938));
#31870=CARTESIAN_POINT('Ctrl Pts',(-9.55017587230574,-0.0155920310208985,
23.2848154240452));
#31871=CARTESIAN_POINT('Ctrl Pts',(-9.55016549375182,-1.36966017015294E-5,
23.2841069671524));
#31872=CARTESIAN_POINT('Origin',(-8.5,0.,22.7));
#31873=CARTESIAN_POINT('',(-9.5501777037735,-7.61342713928581E-6,22.9841069671524));
#31874=CARTESIAN_POINT('',(-9.55005297345142,-1.9100363332081E-5,23.0658930328476));
#31875=CARTESIAN_POINT('',(-9.5501,-1.28600160378464E-16,22.7));
#31876=CARTESIAN_POINT('',(-7.70661869325983,-0.687936125025621,22.8));
#31877=CARTESIAN_POINT('Ctrl Pts',(-9.5501777037735,-7.61342713928581E-6,
22.9841069671524));
#31878=CARTESIAN_POINT('Ctrl Pts',(-9.55011195539345,0.161456714688093,
22.9767637934161));
#31879=CARTESIAN_POINT('Ctrl Pts',(-9.5122535813712,0.322950769429109,22.9694206196799));
#31880=CARTESIAN_POINT('Ctrl Pts',(-9.44037249633203,0.46752981291848,22.9620774459436));
#31881=CARTESIAN_POINT('Ctrl Pts',(-9.36482255869282,0.619488255304342,
22.9543594723273));
#31882=CARTESIAN_POINT('Ctrl Pts',(-9.25168819794997,0.75276091631997,22.9466414987109));
#31883=CARTESIAN_POINT('Ctrl Pts',(-9.11401338581573,0.851981499935064,
22.9389235250945));
#31884=CARTESIAN_POINT('Ctrl Pts',(-8.9763385736815,0.951202083550158,22.9312055514782));
#31885=CARTESIAN_POINT('Ctrl Pts',(-8.8141233101559,1.01637058976472,22.9234875778618));
#31886=CARTESIAN_POINT('Ctrl Pts',(-8.64606976010883,1.03997499101187,22.9157696042454));
#31887=CARTESIAN_POINT('Ctrl Pts',(-8.47801621006176,1.06357939225902,22.9080516306291));
#31888=CARTESIAN_POINT('Ctrl Pts',(-8.30412437349322,1.04561968853876,22.9003336570127));
#31889=CARTESIAN_POINT('Ctrl Pts',(-8.1444440256564,0.988163330864678,22.8926156833964));
#31890=CARTESIAN_POINT('Ctrl Pts',(-7.98476367781957,0.930706973190595,
22.88489770978));
#31891=CARTESIAN_POINT('Ctrl Pts',(-7.83929481871444,0.833753961562689,
22.8771797361636));
#31892=CARTESIAN_POINT('Ctrl Pts',(-7.72480763500893,0.708490009755435,
22.8694617625473));
#31893=CARTESIAN_POINT('Ctrl Pts',(-7.61032045130341,0.583226057948181,
22.8617437889309));
#31894=CARTESIAN_POINT('Ctrl Pts',(-7.52681494299751,0.429651165961579,
22.8540258153145));
#31895=CARTESIAN_POINT('Ctrl Pts',(-7.48392418333634,0.265456912966516,
22.8463078416982));
#31896=CARTESIAN_POINT('Ctrl Pts',(-7.44103342367517,0.101262659971452,
22.8385898680818));
#31897=CARTESIAN_POINT('Ctrl Pts',(-7.43875741265874,-0.0735509540320737,
22.8308718944655));
#31898=CARTESIAN_POINT('Ctrl Pts',(-7.47735339515514,-0.238789147435026,
22.8231539208491));
#31899=CARTESIAN_POINT('Ctrl Pts',(-7.51594937765153,-0.404027340837977,
22.8154359472327));
#31900=CARTESIAN_POINT('Ctrl Pts',(-7.59541735366076,-0.559690113640355,
22.8077179736164));
#31901=CARTESIAN_POINT('Ctrl Pts',(-7.70661869325984,-0.687936125025627,
22.8));
#31902=CARTESIAN_POINT('',(-9.29341948377034,-0.687941604344792,22.8));
#31903=CARTESIAN_POINT('Origin',(-8.5,0.,22.8));
#31904=CARTESIAN_POINT('Ctrl Pts',(-9.29341948377034,-0.687941604344792,
22.8));
#31905=CARTESIAN_POINT('Ctrl Pts',(-9.20135879382107,-0.793916141421131,
22.8063833455655));
#31906=CARTESIAN_POINT('Ctrl Pts',(-9.08793198530623,-0.881431392368405,
22.812766691131));
#31907=CARTESIAN_POINT('Ctrl Pts',(-8.961878029636,-0.943161224705925,22.8191500366966));
#31908=CARTESIAN_POINT('Ctrl Pts',(-8.80946874924919,-1.017797512595,22.8268680103129));
#31909=CARTESIAN_POINT('Ctrl Pts',(-8.63860017390651,-1.05473877390202,
22.8345859839293));
#31910=CARTESIAN_POINT('Ctrl Pts',(-8.46897134575844,-1.04972481267189,
22.8423039575456));
#31911=CARTESIAN_POINT('Ctrl Pts',(-8.29934251761038,-1.04471085144175,
22.850021931162));
#31912=CARTESIAN_POINT('Ctrl Pts',(-8.13095343665695,-0.997741667674461,
22.8577399047784));
#31913=CARTESIAN_POINT('Ctrl Pts',(-7.98321899249379,-0.914233007224389,
22.8654578783947));
#31914=CARTESIAN_POINT('Ctrl Pts',(-7.83548454833064,-0.830724346774318,
22.8731758520111));
#31915=CARTESIAN_POINT('Ctrl Pts',(-7.70840474095778,-0.710676209641467,
22.8808938256275));
#31916=CARTESIAN_POINT('Ctrl Pts',(-7.61663093296774,-0.567929273382309,
22.8886117992438));
#31917=CARTESIAN_POINT('Ctrl Pts',(-7.52485712497771,-0.425182337123151,
22.8963297728602));
#31918=CARTESIAN_POINT('Ctrl Pts',(-7.4683893163705,-0.259736601737684,
22.9040477464765));
#31919=CARTESIAN_POINT('Ctrl Pts',(-7.4537380520049,-0.0906671566566106,
22.9117657200929));
#31920=CARTESIAN_POINT('Ctrl Pts',(-7.43908678763931,0.0784022884244615,
22.9194836937093));
#31921=CARTESIAN_POINT('Ctrl Pts',(-7.46625206751533,0.251095443201141,
22.9272016673256));
#31922=CARTESIAN_POINT('Ctrl Pts',(-7.53210183081577,0.407501772587699,
22.934919640942));
#31923=CARTESIAN_POINT('Ctrl Pts',(-7.5979515941162,0.563908101974257,22.9426376145584));
#31924=CARTESIAN_POINT('Ctrl Pts',(-7.70248584084105,0.704027605970695,
22.9503555881747));
#31925=CARTESIAN_POINT('Ctrl Pts',(-7.83365236534431,0.811705248185335,
22.9580735617911));
#31926=CARTESIAN_POINT('Ctrl Pts',(-7.96481888984757,0.919382890399975,
22.9657915354074));
#31927=CARTESIAN_POINT('Ctrl Pts',(-8.12261769212924,0.994618670832817,
22.9735095090238));
#31928=CARTESIAN_POINT('Ctrl Pts',(-8.28885541853258,1.02873832309996,22.9812274826402));
#31929=CARTESIAN_POINT('Ctrl Pts',(-8.45509314493592,1.06285797536711,22.9889454562565));
#31930=CARTESIAN_POINT('Ctrl Pts',(-8.62976979546093,1.05586149946856,22.9966634298729));
#31931=CARTESIAN_POINT('Ctrl Pts',(-8.79274610833971,1.00855554667633,23.0043814034893));
#31932=CARTESIAN_POINT('Ctrl Pts',(-8.95572242121848,0.961249593884094,
23.0120993771056));
#31933=CARTESIAN_POINT('Ctrl Pts',(-9.10699839645102,0.873634164198181,
23.019817350722));
#31934=CARTESIAN_POINT('Ctrl Pts',(-9.22913273544003,0.755810841613994,
23.0275353243383));
#31935=CARTESIAN_POINT('Ctrl Pts',(-9.35126707442905,0.637987519029806,
23.0352532979547));
#31936=CARTESIAN_POINT('Ctrl Pts',(-9.44425977717454,0.489956303547343,
23.0429712715711));
#31937=CARTESIAN_POINT('Ctrl Pts',(-9.49738929240291,0.328784387440792,
23.0506892451874));
#31938=CARTESIAN_POINT('Ctrl Pts',(-9.53227625056806,0.222952480817186,
23.0557571744075));
#31939=CARTESIAN_POINT('Ctrl Pts',(-9.54997516203667,0.111454620464842,
23.0608251036276));
#31940=CARTESIAN_POINT('Ctrl Pts',(-9.55005297345142,-1.9100363332081E-5,
23.0658930328476));
#31941=CARTESIAN_POINT('Origin',(-8.5,0.,22.1374873996035));
#31942=CARTESIAN_POINT('',(-9.71736782397678,-1.11661056032553E-5,23.7625126003965));
#31943=CARTESIAN_POINT('',(-9.71748305223155,-2.5328750760409E-5,23.7874873996035));
#31944=CARTESIAN_POINT('',(-9.71745,-6.10603367124078E-16,22.1374873996035));
#31945=CARTESIAN_POINT('',(-8.18521110449559,1.17604951161383,24.));
#31946=CARTESIAN_POINT('Ctrl Pts',(-9.71748305223155,-2.53287507604727E-5,
23.7874873996035));
#31947=CARTESIAN_POINT('Ctrl Pts',(-9.71751555392126,-0.0351020131759212,
23.7888631705217));
#31948=CARTESIAN_POINT('Ctrl Pts',(-9.70768391907026,-0.266938163521721,
23.7979569150563));
#31949=CARTESIAN_POINT('Ctrl Pts',(-9.56508040992899,-0.684753960099927,
23.8147686332073));
#31950=CARTESIAN_POINT('Ctrl Pts',(-9.12308448035522,-1.10229305502416,
23.8379225540564));
#31951=CARTESIAN_POINT('Ctrl Pts',(-8.53741087882009,-1.26565644543905,
23.8610764749055));
#31952=CARTESIAN_POINT('Ctrl Pts',(-7.94311335482628,-1.13717113651722,
23.8842303957546));
#31953=CARTESIAN_POINT('Ctrl Pts',(-7.47722227522078,-0.746471900623929,
23.9073843166037));
#31954=CARTESIAN_POINT('Ctrl Pts',(-7.24718526716919,-0.183635135086069,
23.9305382374527));
#31955=CARTESIAN_POINT('Ctrl Pts',(-7.30600778196775,0.421517743452463,
23.9536921583018));
#31956=CARTESIAN_POINT('Ctrl Pts',(-7.64021434930425,0.929509330617972,
23.9768460791509));
#31957=CARTESIAN_POINT('Ctrl Pts',(-7.99510874416175,1.12516550422187,23.9922820263836));
#31958=CARTESIAN_POINT('Ctrl Pts',(-8.18521110449561,1.17604951161383,24.));
#31959=CARTESIAN_POINT('',(-8.81478889550438,1.17604951161383,24.));
#31960=CARTESIAN_POINT('Origin',(-8.5,0.,24.));
#31961=CARTESIAN_POINT('Ctrl Pts',(-9.71736782397678,-1.116610560329E-5,
23.7625126003965));
#31962=CARTESIAN_POINT('Ctrl Pts',(-9.71739662002813,-0.0846136575430615,
23.7658299588182));
#31963=CARTESIAN_POINT('Ctrl Pts',(-9.68844334159764,-0.366027961834239,
23.7768652908563));
#31964=CARTESIAN_POINT('Ctrl Pts',(-9.47383638460599,-0.809275680645407,
23.7956185965108));
#31965=CARTESIAN_POINT('Ctrl Pts',(-8.98431410313225,-1.16992489625058,
23.8187725173598));
#31966=CARTESIAN_POINT('Ctrl Pts',(-8.38311425495986,-1.2608022005996,23.8419264382089));
#31967=CARTESIAN_POINT('Ctrl Pts',(-7.80886700439182,-1.06095217981207,
23.865080359058));
#31968=CARTESIAN_POINT('Ctrl Pts',(-7.39398745671621,-0.616458283433,23.8882342799071));
#31969=CARTESIAN_POINT('Ctrl Pts',(-7.23414244016268,-0.0298154996095495,
23.9113882007562));
#31970=CARTESIAN_POINT('Ctrl Pts',(-7.36619019624783,0.563701731054729,
23.9345421216053));
#31971=CARTESIAN_POINT('Ctrl Pts',(-7.75968252106489,1.02723702411681,23.9576960424544));
#31972=CARTESIAN_POINT('Ctrl Pts',(-8.29136160594112,1.24083426807448,23.9795153352526));
#31973=CARTESIAN_POINT('Ctrl Pts',(-8.657569202316,1.21801597484871,23.9936166544345));
#31974=CARTESIAN_POINT('Ctrl Pts',(-8.81482199187077,1.17607957877116,24.));
#31975=CARTESIAN_POINT('Origin',(-8.5,0.,22.1374873996035));
#31976=CARTESIAN_POINT('',(-9.71737930107838,-1.72188272680729E-5,23.4625126003965));
#31977=CARTESIAN_POINT('',(-9.71750618477853,-2.14937489025574E-5,23.4874873996035));
#31978=CARTESIAN_POINT('',(-9.71745,-6.10603367124078E-16,22.1374873996035));
#31979=CARTESIAN_POINT('Ctrl Pts',(-9.71750618477853,-2.1493748902545E-5,
23.4874873996035));
#31980=CARTESIAN_POINT('Ctrl Pts',(-9.71752840630035,-0.0265897893097531,
23.488529513509));
#31981=CARTESIAN_POINT('Ctrl Pts',(-9.71035853514721,-0.249912895433259,
23.4972896010309));
#31982=CARTESIAN_POINT('Ctrl Pts',(-9.57920081330433,-0.662276356417367,
23.5137676621692));
#31983=CARTESIAN_POINT('Ctrl Pts',(-9.14605438936275,-1.08898948282007,
23.5369215830183));
#31984=CARTESIAN_POINT('Ctrl Pts',(-8.56393485826131,-1.26459349261069,
23.5600755038673));
#31985=CARTESIAN_POINT('Ctrl Pts',(-7.96707264494009,-1.14859601343679,
23.5832294247164));
#31986=CARTESIAN_POINT('Ctrl Pts',(-7.49309767679161,-0.767744800604105,
23.6063833455655));
#31987=CARTESIAN_POINT('Ctrl Pts',(-7.2513034195874,-0.209859997254996,
23.6295372664146));
#31988=CARTESIAN_POINT('Ctrl Pts',(-7.29744499763571,0.396416237173858,
23.6526911872637));
#31989=CARTESIAN_POINT('Ctrl Pts',(-7.62088266214053,0.91128320195394,23.6758451081128));
#31990=CARTESIAN_POINT('Ctrl Pts',(-8.14703521692498,1.21601818778867,23.6989990289619));
#31991=CARTESIAN_POINT('Ctrl Pts',(-8.75457759628112,1.24035261140464,23.722152949811));
#31992=CARTESIAN_POINT('Ctrl Pts',(-9.30341717795882,0.978675249789286,
23.74530687066));
#31993=CARTESIAN_POINT('Ctrl Pts',(-9.64539406535925,0.52028354219972,23.7670850205909));
#31994=CARTESIAN_POINT('Ctrl Pts',(-9.71733322183359,0.161675605360226,
23.7811451969054));
#31995=CARTESIAN_POINT('Ctrl Pts',(-9.71748305223155,-2.53287507604727E-5,
23.7874873996035));
#31996=CARTESIAN_POINT('Ctrl Pts',(-9.71737930107839,-1.72188272682325E-5,
23.4625126003965));
#31997=CARTESIAN_POINT('Ctrl Pts',(-9.71741977805662,-0.0761084070319482,
23.4654963018055));
#31998=CARTESIAN_POINT('Ctrl Pts',(-9.69220303304603,-0.348999015684658,
23.4761979768309));
#31999=CARTESIAN_POINT('Ctrl Pts',(-9.49058703805816,-0.788683553714432,
23.4946176254726));
#32000=CARTESIAN_POINT('Ctrl Pts',(-9.0087325233999,-1.15951526402384,23.5177715463217));
#32001=CARTESIAN_POINT('Ctrl Pts',(-8.40956982850905,-1.26297538057999,
23.5409254671708));
#32002=CARTESIAN_POINT('Ctrl Pts',(-7.8312593464559,-1.07520712710119,23.5640793880199));
#32003=CARTESIAN_POINT('Ctrl Pts',(-7.40715317709645,-0.639507818195355,
23.587233308869));
#32004=CARTESIAN_POINT('Ctrl Pts',(-7.23504558492588,-0.0563449701204428,
23.6103872297181));
#32005=CARTESIAN_POINT('Ctrl Pts',(-7.35462270660441,0.539810414542498,
23.6335411505671));
#32006=CARTESIAN_POINT('Ctrl Pts',(-7.73831135994277,1.011491395628,23.6566950714162));
#32007=CARTESIAN_POINT('Ctrl Pts',(-8.2976371195735,1.24993347528822,23.6798489922653));
#32008=CARTESIAN_POINT('Ctrl Pts',(-8.90362555579596,1.20015450597578,23.7030029131144));
#32009=CARTESIAN_POINT('Ctrl Pts',(-9.41654233415426,0.873632976856196,
23.7261568339635));
#32010=CARTESIAN_POINT('Ctrl Pts',(-9.67490694331657,0.421305905434982,
23.7459933963909));
#32011=CARTESIAN_POINT('Ctrl Pts',(-9.71732962480593,0.112217590029651,
23.7581119852019));
#32012=CARTESIAN_POINT('Ctrl Pts',(-9.71736782397678,-1.116610560329E-5,
23.7625126003965));
#32013=CARTESIAN_POINT('Origin',(-8.5,0.,22.1374873996035));
#32014=CARTESIAN_POINT('',(-9.71739547902908,-2.21443075443251E-5,23.1625126003965));
#32015=CARTESIAN_POINT('',(-9.71752593121431,-1.5879371246656E-5,23.1874873996035));
#32016=CARTESIAN_POINT('',(-9.71745,-6.10603367124078E-16,22.1374873996035));
#32017=CARTESIAN_POINT('Ctrl Pts',(-9.71752593121431,-1.5879371246693E-5,
23.1874873996035));
#32018=CARTESIAN_POINT('Ctrl Pts',(-9.71753796375452,-0.0180768671235083,
23.1881958564963));
#32019=CARTESIAN_POINT('Ctrl Pts',(-9.71285129265438,-0.232889135646274,
23.1966222870055));
#32020=CARTESIAN_POINT('Ctrl Pts',(-9.5928468023976,-0.639507806195877,
23.212766691131));
#32021=CARTESIAN_POINT('Ctrl Pts',(-9.16874064099593,-1.07520710692634,
23.2359206119801));
#32022=CARTESIAN_POINT('Ctrl Pts',(-8.59043016979403,-1.26297535688186,
23.2590745328292));
#32023=CARTESIAN_POINT('Ctrl Pts',(-7.99126748614572,-1.15951524226696,
23.2822284536783));
#32024=CARTESIAN_POINT('Ctrl Pts',(-7.5094129805289,-0.788683538915698,
23.3053823745274));
#32025=CARTESIAN_POINT('Ctrl Pts',(-7.25597705495489,-0.235989999581765,
23.3285362953765));
#32026=CARTESIAN_POINT('Ctrl Pts',(-7.28939927415983,0.371120263926209,
23.3516902162256));
#32027=CARTESIAN_POINT('Ctrl Pts',(-7.60197283833471,0.892654235755761,
23.3748441370746));
#32028=CARTESIAN_POINT('Ctrl Pts',(-8.1216216872399,1.20835186106285,23.3979980579237));
#32029=CARTESIAN_POINT('Ctrl Pts',(-8.72852045485104,1.24541670512988,23.4211519787728));
#32030=CARTESIAN_POINT('Ctrl Pts',(-9.28272489396535,0.99530201851838,23.4443058996219));
#32031=CARTESIAN_POINT('Ctrl Pts',(-9.63962122283735,0.537268329942552,
23.4664177065655));
#32032=CARTESIAN_POINT('Ctrl Pts',(-9.71736383204584,0.170176997010107,
23.4808115398927));
#32033=CARTESIAN_POINT('Ctrl Pts',(-9.71750618477853,-2.1493748902545E-5,
23.4874873996035));
#32034=CARTESIAN_POINT('Ctrl Pts',(-9.71739547902908,-2.21443075442973E-5,
23.1625126003965));
#32035=CARTESIAN_POINT('Ctrl Pts',(-9.71744265125785,-0.0676017388760646,
23.1651626447928));
#32036=CARTESIAN_POINT('Ctrl Pts',(-9.69577268601838,-0.331969805738998,
23.1755306628055));
#32037=CARTESIAN_POINT('Ctrl Pts',(-9.50690234210182,-0.767744815010462,
23.1936166544345));
#32038=CARTESIAN_POINT('Ctrl Pts',(-9.03292736505941,-1.14859603498855,
23.2167705752836));
#32039=CARTESIAN_POINT('Ctrl Pts',(-8.436065140539,-1.2645935163393,23.2399244961327));
#32040=CARTESIAN_POINT('Ctrl Pts',(-7.85394559851473,-1.08898950325348,
23.2630784169817));
#32041=CARTESIAN_POINT('Ctrl Pts',(-7.42079916644579,-0.662276368844085,
23.2862323378308));
#32042=CARTESIAN_POINT('Ctrl Pts',(-7.23650469503931,-0.0828495154220059,
23.3093862586799));
#32043=CARTESIAN_POINT('Ctrl Pts',(-7.34355848256139,0.515681534104197,
23.332540179529));
#32044=CARTESIAN_POINT('Ctrl Pts',(-7.71727509134788,0.995302037194035,
23.3556941003781));
#32045=CARTESIAN_POINT('Ctrl Pts',(-8.27147954086117,1.24541672849857,23.3788480212272));
#32046=CARTESIAN_POINT('Ctrl Pts',(-8.87837831986,1.20835188373602,23.4020019420763));
#32047=CARTESIAN_POINT('Ctrl Pts',(-9.39802717851571,0.892654252505216,
23.4251558629254));
#32048=CARTESIAN_POINT('Ctrl Pts',(-9.67032134156336,0.438327103198321,
23.4453260823654));
#32049=CARTESIAN_POINT('Ctrl Pts',(-9.71731507580687,0.120717515705654,
23.4577783281892));
#32050=CARTESIAN_POINT('Ctrl Pts',(-9.71737930107839,-1.72188272682325E-5,
23.4625126003965));
#32051=CARTESIAN_POINT('Origin',(-8.5,0.,22.1374873996035));
#32052=CARTESIAN_POINT('',(-9.71741556519039,-3.134158932111E-5,22.8625126003965));
#32053=CARTESIAN_POINT('',(-9.71754008709556,-8.82674686203209E-6,22.8874873996035));
#32054=CARTESIAN_POINT('',(-9.71745,-6.10603367124078E-16,22.1374873996035));
#32055=CARTESIAN_POINT('',(-8.8147888955045,1.1760495116138,22.8));
#32056=CARTESIAN_POINT('Ctrl Pts',(-8.81478889550448,1.17604951161381,22.8));
#32057=CARTESIAN_POINT('Ctrl Pts',(-9.00489125583834,1.12516550422183,22.8077179736164));
#32058=CARTESIAN_POINT('Ctrl Pts',(-9.35978561312172,0.929509121580238,
22.8231539208491));
#32059=CARTESIAN_POINT('Ctrl Pts',(-9.66055719692335,0.472338673167377,
22.8439914543146));
#32060=CARTESIAN_POINT('Ctrl Pts',(-9.71730336395768,0.137706364168718,
22.8571110141637));
#32061=CARTESIAN_POINT('Ctrl Pts',(-9.71741556519039,-3.13415893210822E-5,
22.8625126003965));
#32062=CARTESIAN_POINT('',(-8.18517800353966,1.17607954763525,22.8));
#32063=CARTESIAN_POINT('Origin',(-8.5,0.,22.8));
#32064=CARTESIAN_POINT('Ctrl Pts',(-8.18517800353966,1.17607954763525,22.8));
#32065=CARTESIAN_POINT('Ctrl Pts',(-8.34243079339873,1.2180159458478,22.8063833455655));
#32066=CARTESIAN_POINT('Ctrl Pts',(-8.70863838400351,1.24083423778419,22.8204846647474));
#32067=CARTESIAN_POINT('Ctrl Pts',(-9.24031746415369,1.02723700478738,22.8423039575456));
#32068=CARTESIAN_POINT('Ctrl Pts',(-9.62744019623509,0.57120511221857,22.8650830785146));
#32069=CARTESIAN_POINT('Ctrl Pts',(-9.71746386067399,0.187187389102954,
22.8801442258672));
#32070=CARTESIAN_POINT('Ctrl Pts',(-9.71754008709556,-8.82674686206349E-6,
22.8874873996035));
#32071=CARTESIAN_POINT('Origin',(-8.5,0.,22.1374873996035));
#32072=CARTESIAN_POINT('Ctrl Pts',(-9.71754008709556,-8.82674686206349E-6,
22.8874873996035));
#32073=CARTESIAN_POINT('Ctrl Pts',(-9.71754397773668,-0.0095634310334148,
22.8878621994836));
#32074=CARTESIAN_POINT('Ctrl Pts',(-9.71516332688261,-0.215866916824623,
22.8959549729801));
#32075=CARTESIAN_POINT('Ctrl Pts',(-9.6060125223886,-0.616458272121094,
22.9117657200929));
#32076=CARTESIAN_POINT('Ctrl Pts',(-9.19113298264395,-1.06095215983846,
22.934919640942));
#32077=CARTESIAN_POINT('Ctrl Pts',(-8.61688574282532,-1.26080217699431,
22.9580735617911));
#32078=CARTESIAN_POINT('Ctrl Pts',(-8.01568590595785,-1.16992487427985,
22.9812274826402));
#32079=CARTESIAN_POINT('Ctrl Pts',(-7.52616363366338,-0.809275665471485,
23.0043814034893));
#32080=CARTESIAN_POINT('Ctrl Pts',(-7.26119741948789,-0.262016286526366,
23.0275353243383));
#32081=CARTESIAN_POINT('Ctrl Pts',(-7.28188559259607,0.345661188566822,
23.0506892451874));
#32082=CARTESIAN_POINT('Ctrl Pts',(-7.58345768304373,0.873632960464764,
23.0738431660365));
#32083=CARTESIAN_POINT('Ctrl Pts',(-8.09637445177758,1.20015448345588,23.0969970868856));
#32084=CARTESIAN_POINT('Ctrl Pts',(-8.70236287662956,1.24993345183503,23.1201510077347));
#32085=CARTESIAN_POINT('Ctrl Pts',(-9.26168862576517,1.01149137664845,23.1433049285838));
#32086=CARTESIAN_POINT('Ctrl Pts',(-9.63363727901798,0.554242760737588,
23.1657503925401));
#32087=CARTESIAN_POINT('Ctrl Pts',(-9.7174068805104,0.178680660921264,23.18047788288));
#32088=CARTESIAN_POINT('Ctrl Pts',(-9.71752593121431,-1.5879371246693E-5,
23.1874873996035));
#32089=CARTESIAN_POINT('Ctrl Pts',(-9.71741556519039,-3.13415893210822E-5,
22.8625126003965));
#32090=CARTESIAN_POINT('Ctrl Pts',(-9.71746368096762,-0.0590980435010754,
22.8648289877801));
#32091=CARTESIAN_POINT('Ctrl Pts',(-9.69914933317854,-0.314939569855699,
22.87486334878));
#32092=CARTESIAN_POINT('Ctrl Pts',(-9.5227777403229,-0.746471923361528,
22.8926156833964));
#32093=CARTESIAN_POINT('Ctrl Pts',(-9.05688665443706,-1.13717116763217,
22.9157696042454));
#32094=CARTESIAN_POINT('Ctrl Pts',(-8.46258911977101,-1.2656564697317,22.9389235250945));
#32095=CARTESIAN_POINT('Ctrl Pts',(-7.87691550790518,-1.10229307735719,
22.9620774459436));
#32096=CARTESIAN_POINT('Ctrl Pts',(-7.43491956993902,-0.684753972836506,
22.9852313667927));
#32097=CARTESIAN_POINT('Ctrl Pts',(-7.23851903592649,-0.109317603314454,
23.0083852876418));
#32098=CARTESIAN_POINT('Ctrl Pts',(-7.33300252317075,0.49132599619855,23.0315392084909));
#32099=CARTESIAN_POINT('Ctrl Pts',(-7.69658280697753,0.978675268097788,
23.05469312934));
#32100=CARTESIAN_POINT('Ctrl Pts',(-8.24542239893397,1.24035263469515,23.077847050189));
#32101=CARTESIAN_POINT('Ctrl Pts',(-8.85296478970154,1.21601821059452,23.1010009710381));
#32102=CARTESIAN_POINT('Ctrl Pts',(-9.37911735435305,0.911283219057196,
23.1241548918872));
#32103=CARTESIAN_POINT('Ctrl Pts',(-9.66553649178147,0.455344507747716,
23.14465876834));
#32104=CARTESIAN_POINT('Ctrl Pts',(-9.71730526713794,0.129216672397783,
23.1574446711764));
#32105=CARTESIAN_POINT('Ctrl Pts',(-9.71739547902908,-2.21443075442973E-5,
23.1625126003965));
#32106=CARTESIAN_POINT('Ctrl Pts',(-7.70661869325984,-0.687936125025627,
22.8));
#32107=CARTESIAN_POINT('Ctrl Pts',(-7.59541735366076,-0.559690113640355,
22.8077179736164));
#32108=CARTESIAN_POINT('Ctrl Pts',(-7.43648140164231,-0.248364568035598,
22.8231539208491));
#32109=CARTESIAN_POINT('Ctrl Pts',(-7.4433094346916,0.276076273974975,22.8463078416982));
#32110=CARTESIAN_POINT('Ctrl Pts',(-7.69382595960932,0.736800949934783,
22.8694617625473));
#32111=CARTESIAN_POINT('Ctrl Pts',(-8.13023253692469,1.0276599848185,22.8926156833964));
#32112=CARTESIAN_POINT('Ctrl Pts',(-8.65190804663029,1.08153909597928,22.9157696042454));
#32113=CARTESIAN_POINT('Ctrl Pts',(-9.13855383720711,0.886033577335599,
22.9389235250945));
#32114=CARTESIAN_POINT('Ctrl Pts',(-9.47795691943568,0.486215594288713,
22.9620774459436));
#32115=CARTESIAN_POINT('Ctrl Pts',(-9.59185346304236,-0.0257170769795772,
22.9852313667927));
#32116=CARTESIAN_POINT('Ctrl Pts',(-9.45398065609287,-0.531720260835648,
23.0083852876418));
#32117=CARTESIAN_POINT('Ctrl Pts',(-9.09613022717517,-0.915114265921696,
23.0315392084909));
#32118=CARTESIAN_POINT('Ctrl Pts',(-8.60081869361441,-1.08749301085197,
23.05469312934));
#32119=CARTESIAN_POINT('Ctrl Pts',(-8.08225945200734,-1.00910765163355,
23.077847050189));
#32120=CARTESIAN_POINT('Ctrl Pts',(-7.66002663904875,-0.698033082518055,
23.1010009710381));
#32121=CARTESIAN_POINT('Ctrl Pts',(-7.43148253333133,-0.225999673482555,
23.1241548918872));
#32122=CARTESIAN_POINT('Ctrl Pts',(-7.44932692166836,0.298146793801815,
23.1473088127363));
#32123=CARTESIAN_POINT('Ctrl Pts',(-7.70944508026138,0.753543859529384,
23.1704627335854));
#32124=CARTESIAN_POINT('Ctrl Pts',(-8.15185659518801,1.03518191554233,23.1936166544345));
#32125=CARTESIAN_POINT('Ctrl Pts',(-8.67454618813808,1.0781182946092,23.2167705752836));
#32126=CARTESIAN_POINT('Ctrl Pts',(-9.15698733082756,0.87245233448481,23.2399244961327));
#32127=CARTESIAN_POINT('Ctrl Pts',(-9.48793434902992,0.465608366400854,
23.2630784169817));
#32128=CARTESIAN_POINT('Ctrl Pts',(-9.59107446412167,-0.0485998209482193,
23.2862323378308));
#32129=CARTESIAN_POINT('Ctrl Pts',(-9.44262468865063,-0.551601418773905,
23.3093862586799));
#32130=CARTESIAN_POINT('Ctrl Pts',(-9.07681592435815,-0.927409735909772,
23.332540179529));
#32131=CARTESIAN_POINT('Ctrl Pts',(-8.57799968894059,-1.08936746664063,
23.3556941003781));
#32132=CARTESIAN_POINT('Ctrl Pts',(-8.06119757460399,-1.00012892184856,
23.3788480212272));
#32133=CARTESIAN_POINT('Ctrl Pts',(-7.64557852137944,-0.680271538227749,
23.4020019420763));
#32134=CARTESIAN_POINT('Ctrl Pts',(-7.4269797572041,-0.203550945468653,
23.4251558629254));
#32135=CARTESIAN_POINT('Ctrl Pts',(-7.45580777674256,0.320106278819592,
23.4483097837744));
#32136=CARTESIAN_POINT('Ctrl Pts',(-7.72541515260198,0.769950480896237,
23.4714637046235));
#32137=CARTESIAN_POINT('Ctrl Pts',(-8.17363335970316,1.04225248618185,23.4946176254726));
#32138=CARTESIAN_POINT('Ctrl Pts',(-8.69710816020295,1.07422241739446,23.5177715463217));
#32139=CARTESIAN_POINT('Ctrl Pts',(-9.17513196529879,0.85848835652072,23.5409254671708));
#32140=CARTESIAN_POINT('Ctrl Pts',(-9.49747769080951,0.444796228840474,
23.5640793880199));
#32141=CARTESIAN_POINT('Ctrl Pts',(-9.58981592249665,-0.0714610657623065,
23.587233308869));
#32142=CARTESIAN_POINT('Ctrl Pts',(-9.43085446962986,-0.571240216743092,
23.6103872297181));
#32143=CARTESIAN_POINT('Ctrl Pts',(-9.05724811225909,-0.939297594077255,
23.6335411505671));
#32144=CARTESIAN_POINT('Ctrl Pts',(-8.55514640819762,-1.090763174332,23.6566950714162));
#32145=CARTESIAN_POINT('Ctrl Pts',(-8.0403285428162,-0.990710644141418,
23.6798489922653));
#32146=CARTESIAN_POINT('Ctrl Pts',(-7.63150591022126,-0.662211027240847,
23.7030029131144));
#32147=CARTESIAN_POINT('Ctrl Pts',(-7.42294855715531,-0.181012758731342,
23.7261568339635));
#32148=CARTESIAN_POINT('Ctrl Pts',(-7.46274753954353,0.341925081651212,
23.7493107548126));
#32149=CARTESIAN_POINT('Ctrl Pts',(-7.74172564254284,0.786018719760016,
23.7724646756617));
#32150=CARTESIAN_POINT('Ctrl Pts',(-8.19555355972969,1.04886500389904,23.7956185965107));
#32151=CARTESIAN_POINT('Ctrl Pts',(-8.71958350146191,1.06985443117665,23.8187725173598));
#32152=CARTESIAN_POINT('Ctrl Pts',(-9.19297989944109,0.844147094175308,
23.8419264382089));
#32153=CARTESIAN_POINT('Ctrl Pts',(-9.50658263369233,0.423788589976583,
23.865080359058));
#32154=CARTESIAN_POINT('Ctrl Pts',(-9.588078471842,-0.0942908643321087,
23.8882342799071));
#32155=CARTESIAN_POINT('Ctrl Pts',(-9.41867504905042,-0.5906280615228,23.9113882007562));
#32156=CARTESIAN_POINT('Ctrl Pts',(-9.03743563417062,-0.950772464644027,
23.9345421216053));
#32157=CARTESIAN_POINT('Ctrl Pts',(-8.53226840022093,-1.09168001425565,
23.9576960424544));
#32158=CARTESIAN_POINT('Ctrl Pts',(-8.01966268339815,-0.980856224450063,
23.9808499633034));
#32159=CARTESIAN_POINT('Ctrl Pts',(-7.61781273252235,-0.643862288262505,
24.0040038841525));
#32160=CARTESIAN_POINT('Ctrl Pts',(-7.41939648367848,-0.158392751533025,
24.0271578050016));
#32161=CARTESIAN_POINT('Ctrl Pts',(-7.47013328830288,0.363576148835214,
24.0503117258507));
#32162=CARTESIAN_POINT('Ctrl Pts',(-7.758400006739,0.801739494913083,24.0734656466998));
#32163=CARTESIAN_POINT('Ctrl Pts',(-8.06451081542918,0.970500879693935,
24.0889015939325));
#32164=CARTESIAN_POINT('Ctrl Pts',(-8.22848181102373,1.0143903997254,24.0966195675489));
#32165=CARTESIAN_POINT('Ctrl Pts',(-7.66447275106926,-0.724480616192512,
22.7677934774837));
#32166=CARTESIAN_POINT('Ctrl Pts',(-7.54736418225966,-0.589421929822215,
22.7755114511001));
#32167=CARTESIAN_POINT('Ctrl Pts',(-7.37998524653481,-0.261558171965623,
22.7909473983328));
#32168=CARTESIAN_POINT('Ctrl Pts',(-7.38717599784293,0.290741977066652,
22.8141013191819));
#32169=CARTESIAN_POINT('Ctrl Pts',(-7.65100044278255,0.775941234660551,
22.837255240031));
#32170=CARTESIAN_POINT('Ctrl Pts',(-8.11058977752221,1.0822512613507,22.8604091608801));
#32171=CARTESIAN_POINT('Ctrl Pts',(-8.65997769447449,1.13899253460802,22.8835630817292));
#32172=CARTESIAN_POINT('Ctrl Pts',(-9.1724750461893,0.933101386486192,22.9067170025782));
#32173=CARTESIAN_POINT('Ctrl Pts',(-9.52990787346151,0.512044302571802,
22.9298709234273));
#32174=CARTESIAN_POINT('Ctrl Pts',(-9.64985482070358,-0.0270832176114321,
22.9530248442764));
#32175=CARTESIAN_POINT('Ctrl Pts',(-9.50465794485812,-0.559966264597463,
22.9761787651255));
#32176=CARTESIAN_POINT('Ctrl Pts',(-9.12779781233143,-0.963726897227285,
22.9993326859746));
#32177=CARTESIAN_POINT('Ctrl Pts',(-8.60617437668471,-1.14526273289942,
23.0224866068237));
#32178=CARTESIAN_POINT('Ctrl Pts',(-8.06006826999085,-1.06271339251565,
23.0456405276728));
#32179=CARTESIAN_POINT('Ctrl Pts',(-7.61540563725363,-0.735113943502532,
23.0687944485218));
#32180=CARTESIAN_POINT('Ctrl Pts',(-7.37472082871686,-0.238005211163826,
23.0919483693709));
#32181=CARTESIAN_POINT('Ctrl Pts',(-7.39351314531093,0.313984925390151,
23.11510229022));
#32182=CARTESIAN_POINT('Ctrl Pts',(-7.66744928118883,0.793573559841177,
23.1382562110691));
#32183=CARTESIAN_POINT('Ctrl Pts',(-8.13336254738453,1.09017277151351,23.1614101319182));
#32184=CARTESIAN_POINT('Ctrl Pts',(-8.68381841763523,1.13539001368448,23.1845640527673));
#32185=CARTESIAN_POINT('Ctrl Pts',(-9.19188776247343,0.918798681872689,
23.2077179736164));
#32186=CARTESIAN_POINT('Ctrl Pts',(-9.54041532332131,0.490342379071769,
23.2308718944654));
#32187=CARTESIAN_POINT('Ctrl Pts',(-9.64903443986073,-0.0511815369865916,
23.2540258153145));
#32188=CARTESIAN_POINT('Ctrl Pts',(-9.49269872656629,-0.580903547914563,
23.2771797361636));
#32189=CARTESIAN_POINT('Ctrl Pts',(-9.10745749657075,-0.976675526248629,
23.3003336570127));
#32190=CARTESIAN_POINT('Ctrl Pts',(-8.58214318255841,-1.14723676338771,
23.3234875778618));
#32191=CARTESIAN_POINT('Ctrl Pts',(-8.0378875451179,-1.05325769532136,23.3466414987109));
#32192=CARTESIAN_POINT('Ctrl Pts',(-7.60019000776259,-0.716408871790399,
23.36979541956));
#32193=CARTESIAN_POINT('Ctrl Pts',(-7.36997885645436,-0.214363963506357,
23.3929493404091));
#32194=CARTESIAN_POINT('Ctrl Pts',(-7.40033827588165,0.337110940521798,
23.4161032612582));
#32195=CARTESIAN_POINT('Ctrl Pts',(-7.68426771451289,0.810851732516078,
23.4392571821072));
#32196=CARTESIAN_POINT('Ctrl Pts',(-8.15629613554874,1.09761894447552,23.4624111029563));
#32197=CARTESIAN_POINT('Ctrl Pts',(-8.70757892508565,1.13128717997293,23.4855650238054));
#32198=CARTESIAN_POINT('Ctrl Pts',(-9.21099627485431,0.90409291051994,23.5087189446545));
#32199=CARTESIAN_POINT('Ctrl Pts',(-9.55046562578617,0.468424660702981,
23.5318728655036));
#32200=CARTESIAN_POINT('Ctrl Pts',(-9.64770904208202,-0.075257215130723,
23.5550267863527));
#32201=CARTESIAN_POINT('Ctrl Pts',(-9.48030325085468,-0.601585596634517,
23.5781807072018));
#32202=CARTESIAN_POINT('Ctrl Pts',(-9.08685020462698,-0.989194890324859,
23.6013346280509));
#32203=CARTESIAN_POINT('Ctrl Pts',(-8.55807589155219,-1.14870661375823,
23.6244885488999));
#32204=CARTESIAN_POINT('Ctrl Pts',(-8.01590991019083,-1.04333910057321,
23.647642469749));
#32205=CARTESIAN_POINT('Ctrl Pts',(-7.58536983241137,-0.697388951695266,
23.6707963905981));
#32206=CARTESIAN_POINT('Ctrl Pts',(-7.36573351129933,-0.190628504905893,
23.6939503114472));
#32207=CARTESIAN_POINT('Ctrl Pts',(-7.40764669224092,0.360088800158761,
23.7171042322963));
#32208=CARTESIAN_POINT('Ctrl Pts',(-7.7014446490754,0.82777354715799,23.7402581531454));
#32209=CARTESIAN_POINT('Ctrl Pts',(-8.17938077879479,1.10458273186225,23.7634120739945));
#32210=CARTESIAN_POINT('Ctrl Pts',(-8.73124819973498,1.12668715791932,23.7865659948435));
#32211=CARTESIAN_POINT('Ctrl Pts',(-9.22979232561366,0.888989812713301,
23.8097199156926));
#32212=CARTESIAN_POINT('Ctrl Pts',(-9.560054240761,0.446301055625118,23.8328738365417));
#32213=CARTESIAN_POINT('Ctrl Pts',(-9.64587929470419,-0.0992997765455415,
23.8560277573908));
#32214=CARTESIAN_POINT('Ctrl Pts',(-9.46747683600994,-0.622003361048509,
23.8791816782399));
#32215=CARTESIAN_POINT('Ctrl Pts',(-9.06598524956549,-1.00127932810407,
23.902335599089));
#32216=CARTESIAN_POINT('Ctrl Pts',(-8.53398255975398,-1.14967215798345,
23.9254895199381));
#32217=CARTESIAN_POINT('Ctrl Pts',(-7.99414624054086,-1.03296119513911,
23.9486434407871));
#32218=CARTESIAN_POINT('Ctrl Pts',(-7.57094924675516,-0.67806549238298,
23.9717973616362));
#32219=CARTESIAN_POINT('Ctrl Pts',(-7.36199274484205,-0.166806879384039,
23.9949512824853));
#32220=CARTESIAN_POINT('Ctrl Pts',(-7.41542478619117,0.382890013707631,
24.0181052033344));
#32221=CARTESIAN_POINT('Ctrl Pts',(-7.71900478759408,0.844329440148046,
24.0412591241835));
#32222=CARTESIAN_POINT('Ctrl Pts',(-8.04137679167337,1.02205575453658,24.0566950714162));
#32223=CARTESIAN_POINT('Ctrl Pts',(-8.21405824218102,1.06827677035487,24.0644130450326));
#32224=CARTESIAN_POINT('Ctrl Pts',(-7.62232680887869,-0.761025107359397,
22.7355869549674));
#32225=CARTESIAN_POINT('Ctrl Pts',(-7.49931101085856,-0.619153746004075,
22.7433049285838));
#32226=CARTESIAN_POINT('Ctrl Pts',(-7.32348909142731,-0.274751775895648,
22.7587408758165));
#32227=CARTESIAN_POINT('Ctrl Pts',(-7.33104256099426,0.305407680158331,
22.7818947966656));
#32228=CARTESIAN_POINT('Ctrl Pts',(-7.60817492595577,0.815081519386318,
22.8050487175147));
#32229=CARTESIAN_POINT('Ctrl Pts',(-8.09094701811972,1.13684253788289,22.8282026383638));
#32230=CARTESIAN_POINT('Ctrl Pts',(-8.66804734231868,1.19644597323676,22.8513565592128));
#32231=CARTESIAN_POINT('Ctrl Pts',(-9.2063962551715,0.980169195636786,22.8745104800619));
#32232=CARTESIAN_POINT('Ctrl Pts',(-9.58185882748734,0.537873010854892,
22.897664400911));
#32233=CARTESIAN_POINT('Ctrl Pts',(-9.70785617836479,-0.0284493582432865,
22.9208183217601));
#32234=CARTESIAN_POINT('Ctrl Pts',(-9.55533523362336,-0.588212268359279,
22.9439722426092));
#32235=CARTESIAN_POINT('Ctrl Pts',(-9.15946539748769,-1.01233952853287,
22.9671261634583));
#32236=CARTESIAN_POINT('Ctrl Pts',(-8.61153005975502,-1.20303245494687,
22.9902800843074));
#32237=CARTESIAN_POINT('Ctrl Pts',(-8.03787708797435,-1.11631913339775,
23.0134340051565));
#32238=CARTESIAN_POINT('Ctrl Pts',(-7.5707846354585,-0.772194804487008,
23.0365879260055));
#32239=CARTESIAN_POINT('Ctrl Pts',(-7.31795912410237,-0.250010748845096,
23.0597418468546));
#32240=CARTESIAN_POINT('Ctrl Pts',(-7.3376993689535,0.329823056978487,23.0828957677037));
#32241=CARTESIAN_POINT('Ctrl Pts',(-7.62545348211628,0.83360326015297,23.1060496885528));
#32242=CARTESIAN_POINT('Ctrl Pts',(-8.11486849958106,1.1451636274847,23.1292036094019));
#32243=CARTESIAN_POINT('Ctrl Pts',(-8.69309064713239,1.19266173275976,23.152357530251));
#32244=CARTESIAN_POINT('Ctrl Pts',(-9.2267881941193,0.965145029260567,23.1755114511001));
#32245=CARTESIAN_POINT('Ctrl Pts',(-9.59289629761269,0.515076391742683,
23.1986653719492));
#32246=CARTESIAN_POINT('Ctrl Pts',(-9.70699441559979,-0.0537632530249641,
23.2218192927982));
#32247=CARTESIAN_POINT('Ctrl Pts',(-9.54277276448194,-0.61020567705522,
23.2449732136473));
#32248=CARTESIAN_POINT('Ctrl Pts',(-9.13809906878334,-1.02594131658749,
23.2681271344964));
#32249=CARTESIAN_POINT('Ctrl Pts',(-8.58628667617622,-1.20510606013478,
23.2912810553455));
#32250=CARTESIAN_POINT('Ctrl Pts',(-8.01457751563181,-1.10638646879416,
23.3144349761946));
#32251=CARTESIAN_POINT('Ctrl Pts',(-7.55480149414575,-0.752546205353048,
23.3375888970437));
#32252=CARTESIAN_POINT('Ctrl Pts',(-7.31297795570463,-0.225176981544062,
23.3607428178928));
#32253=CARTESIAN_POINT('Ctrl Pts',(-7.34486877502074,0.354115602224003,
23.3838967387419));
#32254=CARTESIAN_POINT('Ctrl Pts',(-7.6431202764238,0.85175298413592,23.4070506595909));
#32255=CARTESIAN_POINT('Ctrl Pts',(-8.13895891139432,1.15298540276918,23.43020458044));
#32256=CARTESIAN_POINT('Ctrl Pts',(-8.71804968996834,1.18835194255141,23.4533585012891));
#32257=CARTESIAN_POINT('Ctrl Pts',(-9.24686058440983,0.94969746451916,23.4765124221382));
#32258=CARTESIAN_POINT('Ctrl Pts',(-9.60345356076283,0.492053092565487,
23.4996663429873));
#32259=CARTESIAN_POINT('Ctrl Pts',(-9.7056021616674,-0.079053364499139,
23.5228202638364));
#32260=CARTESIAN_POINT('Ctrl Pts',(-9.52975203207951,-0.631930976525942,
23.5459741846855));
#32261=CARTESIAN_POINT('Ctrl Pts',(-9.11645229699486,-1.03909218657246,
23.5691281055346));
#32262=CARTESIAN_POINT('Ctrl Pts',(-8.56100537490675,-1.20665005318446,
23.5922820263836));
#32263=CARTESIAN_POINT('Ctrl Pts',(-7.99149127756545,-1.095967557005,23.6154359472327));
#32264=CARTESIAN_POINT('Ctrl Pts',(-7.53923375460149,-0.732566876149685,
23.6385898680818));
#32265=CARTESIAN_POINT('Ctrl Pts',(-7.30851846544336,-0.200244251080445,
23.6617437889309));
#32266=CARTESIAN_POINT('Ctrl Pts',(-7.35254584493832,0.37825251866631,23.68489770978));
#32267=CARTESIAN_POINT('Ctrl Pts',(-7.66116365560797,0.869528374555965,
23.7080516306291));
#32268=CARTESIAN_POINT('Ctrl Pts',(-8.16320799785988,1.16030045982546,23.7312055514782));
#32269=CARTESIAN_POINT('Ctrl Pts',(-8.74291289800805,1.18351988466198,23.7543594723273));
#32270=CARTESIAN_POINT('Ctrl Pts',(-9.26660475178623,0.933832531251294,
23.7775133931763));
#32271=CARTESIAN_POINT('Ctrl Pts',(-9.61352584782966,0.468813521273654,
23.8006673140254));
#32272=CARTESIAN_POINT('Ctrl Pts',(-9.70368011756638,-0.104308688758975,
23.8238212348745));
#32273=CARTESIAN_POINT('Ctrl Pts',(-9.51627862296947,-0.653378660574218,
23.8469751557236));
#32274=CARTESIAN_POINT('Ctrl Pts',(-9.09453486496036,-1.05178619156412,
23.8701290765727));
#32275=CARTESIAN_POINT('Ctrl Pts',(-8.53569671928704,-1.20766430171125,
23.8932829974218));
#32276=CARTESIAN_POINT('Ctrl Pts',(-7.96862979768357,-1.08506616582817,
23.9164369182709));
#32277=CARTESIAN_POINT('Ctrl Pts',(-7.52408576098797,-0.712268696503455,
23.93959083912));
#32278=CARTESIAN_POINT('Ctrl Pts',(-7.30458900600562,-0.175221007235054,
23.962744759969));
#32279=CARTESIAN_POINT('Ctrl Pts',(-7.36071628407946,0.402203878580047,
23.9858986808181));
#32280=CARTESIAN_POINT('Ctrl Pts',(-7.67960956844917,0.886919385383009,
24.0090526016672));
#32281=CARTESIAN_POINT('Ctrl Pts',(-8.01824276791756,1.07361062937922,24.0244885488999));
#32282=CARTESIAN_POINT('Ctrl Pts',(-8.19963467333832,1.12216314098435,24.0322065225163));
#32283=CARTESIAN_POINT('Ctrl Pts',(-7.58018086668812,-0.797569598526283,
22.7033804324511));
#32284=CARTESIAN_POINT('Ctrl Pts',(-7.45125783945747,-0.648885562185935,
22.7110984060675));
#32285=CARTESIAN_POINT('Ctrl Pts',(-7.26699293631981,-0.287945379825673,
22.7265343533002));
#32286=CARTESIAN_POINT('Ctrl Pts',(-7.27490912414559,0.320073383250008,
22.7496882741493));
#32287=CARTESIAN_POINT('Ctrl Pts',(-7.565349409129,0.854221804112086,22.7728421949984));
#32288=CARTESIAN_POINT('Ctrl Pts',(-8.07130425871723,1.19143381441509,22.7959961158475));
#32289=CARTESIAN_POINT('Ctrl Pts',(-8.67611699016288,1.25389941186551,22.8191500366966));
#32290=CARTESIAN_POINT('Ctrl Pts',(-9.24031746415369,1.02723700478738,22.8423039575456));
#32291=CARTESIAN_POINT('Ctrl Pts',(-9.63380978151316,0.563701719137981,
22.8654578783947));
#32292=CARTESIAN_POINT('Ctrl Pts',(-9.76585753602602,-0.0298154988751415,
22.8886117992438));
#32293=CARTESIAN_POINT('Ctrl Pts',(-9.6060125223886,-0.616458272121094,
22.9117657200929));
#32294=CARTESIAN_POINT('Ctrl Pts',(-9.19113298264395,-1.06095215983846,
22.934919640942));
#32295=CARTESIAN_POINT('Ctrl Pts',(-8.61688574282532,-1.26080217699431,
22.9580735617911));
#32296=CARTESIAN_POINT('Ctrl Pts',(-8.01568590595785,-1.16992487427985,
22.9812274826402));
#32297=CARTESIAN_POINT('Ctrl Pts',(-7.52616363366338,-0.809275665471485,
23.0043814034893));
#32298=CARTESIAN_POINT('Ctrl Pts',(-7.26119741948789,-0.262016286526366,
23.0275353243383));
#32299=CARTESIAN_POINT('Ctrl Pts',(-7.28188559259607,0.345661188566822,
23.0506892451874));
#32300=CARTESIAN_POINT('Ctrl Pts',(-7.58345768304373,0.873632960464764,
23.0738431660365));
#32301=CARTESIAN_POINT('Ctrl Pts',(-8.09637445177758,1.20015448345588,23.0969970868856));
#32302=CARTESIAN_POINT('Ctrl Pts',(-8.70236287662956,1.24993345183503,23.1201510077347));
#32303=CARTESIAN_POINT('Ctrl Pts',(-9.26168862576517,1.01149137664845,23.1433049285838));
#32304=CARTESIAN_POINT('Ctrl Pts',(-9.64537727190408,0.539810404413598,
23.1664588494329));
#32305=CARTESIAN_POINT('Ctrl Pts',(-9.76495439133885,-0.0563449690633367,
23.189612770282));
#32306=CARTESIAN_POINT('Ctrl Pts',(-9.5928468023976,-0.639507806195877,
23.212766691131));
#32307=CARTESIAN_POINT('Ctrl Pts',(-9.16874064099593,-1.07520710692634,
23.2359206119801));
#32308=CARTESIAN_POINT('Ctrl Pts',(-8.59043016979403,-1.26297535688186,
23.2590745328292));
#32309=CARTESIAN_POINT('Ctrl Pts',(-7.99126748614572,-1.15951524226696,
23.2822284536783));
#32310=CARTESIAN_POINT('Ctrl Pts',(-7.5094129805289,-0.788683538915698,
23.3053823745274));
#32311=CARTESIAN_POINT('Ctrl Pts',(-7.25597705495489,-0.235989999581765,
23.3285362953765));
#32312=CARTESIAN_POINT('Ctrl Pts',(-7.28939927415983,0.371120263926209,
23.3516902162256));
#32313=CARTESIAN_POINT('Ctrl Pts',(-7.60197283833471,0.892654235755761,
23.3748441370746));
#32314=CARTESIAN_POINT('Ctrl Pts',(-8.1216216872399,1.20835186106285,23.3979980579237));
#32315=CARTESIAN_POINT('Ctrl Pts',(-8.72852045485104,1.24541670512988,23.4211519787728));
#32316=CARTESIAN_POINT('Ctrl Pts',(-9.28272489396535,0.99530201851838,23.4443058996219));
#32317=CARTESIAN_POINT('Ctrl Pts',(-9.65644149573949,0.515681524427994,
23.467459820471));
#32318=CARTESIAN_POINT('Ctrl Pts',(-9.76349528125278,-0.0828495138675556,
23.4906137413201));
#32319=CARTESIAN_POINT('Ctrl Pts',(-9.57920081330433,-0.662276356417367,
23.5137676621692));
#32320=CARTESIAN_POINT('Ctrl Pts',(-9.14605438936275,-1.08898948282007,
23.5369215830183));
#32321=CARTESIAN_POINT('Ctrl Pts',(-8.56393485826131,-1.26459349261069,
23.5600755038673));
#32322=CARTESIAN_POINT('Ctrl Pts',(-7.96707264494009,-1.14859601343679,
23.5832294247164));
#32323=CARTESIAN_POINT('Ctrl Pts',(-7.49309767679161,-0.767744800604105,
23.6063833455655));
#32324=CARTESIAN_POINT('Ctrl Pts',(-7.2513034195874,-0.209859997254996,
23.6295372664146));
#32325=CARTESIAN_POINT('Ctrl Pts',(-7.29744499763571,0.396416237173858,
23.6526911872637));
#32326=CARTESIAN_POINT('Ctrl Pts',(-7.62088266214053,0.91128320195394,23.6758451081128));
#32327=CARTESIAN_POINT('Ctrl Pts',(-8.14703521692498,1.21601818778867,23.6989990289619));
#32328=CARTESIAN_POINT('Ctrl Pts',(-8.75457759628112,1.24035261140464,23.722152949811));
#32329=CARTESIAN_POINT('Ctrl Pts',(-9.30341717795882,0.978675249789286,
23.74530687066));
#32330=CARTESIAN_POINT('Ctrl Pts',(-9.66699745489832,0.491325986922189,
23.7684607915091));
#32331=CARTESIAN_POINT('Ctrl Pts',(-9.76148094042856,-0.109317600972408,
23.7916147123582));
#32332=CARTESIAN_POINT('Ctrl Pts',(-9.56508040992899,-0.684753960099927,
23.8147686332073));
#32333=CARTESIAN_POINT('Ctrl Pts',(-9.12308448035522,-1.10229305502416,
23.8379225540564));
#32334=CARTESIAN_POINT('Ctrl Pts',(-8.53741087882009,-1.26565644543905,
23.8610764749055));
#32335=CARTESIAN_POINT('Ctrl Pts',(-7.94311335482628,-1.13717113651722,
23.8842303957546));
#32336=CARTESIAN_POINT('Ctrl Pts',(-7.47722227522078,-0.746471900623929,
23.9073843166037));
#32337=CARTESIAN_POINT('Ctrl Pts',(-7.24718526716919,-0.183635135086069,
23.9305382374527));
#32338=CARTESIAN_POINT('Ctrl Pts',(-7.30600778196775,0.421517743452463,
23.9536921583018));
#32339=CARTESIAN_POINT('Ctrl Pts',(-7.64021434930425,0.929509330617972,
23.9768460791509));
#32340=CARTESIAN_POINT('Ctrl Pts',(-7.99510874416175,1.12516550422187,23.9922820263836));
#32341=CARTESIAN_POINT('Ctrl Pts',(-8.18521110449561,1.17604951161383,24.));
#32342=CARTESIAN_POINT('Ctrl Pts',(-8.18521110449561,1.17604951161383,24.));
#32343=CARTESIAN_POINT('Ctrl Pts',(-8.13719967674948,1.15963874913234,24.));
#32344=CARTESIAN_POINT('Ctrl Pts',(-8.09039244203195,1.14022118863296,24.));
#32345=CARTESIAN_POINT('Ctrl Pts',(-8.0450272420164,1.11798779976491,24.));
#32346=CARTESIAN_POINT('Ctrl Pts',(-7.99968369246786,1.09576502174509,24.));
#32347=CARTESIAN_POINT('Ctrl Pts',(-7.95577990341876,1.07072840198051,24.));
#32348=CARTESIAN_POINT('Ctrl Pts',(-7.91358061464719,1.04302439914058,24.));
#32349=CARTESIAN_POINT('Ctrl Pts',(-7.87480187129976,1.01756599813196,24.));
#32350=CARTESIAN_POINT('Ctrl Pts',(-7.83746227877575,0.989854238462992,
24.));
#32351=CARTESIAN_POINT('Ctrl Pts',(-7.80179731248717,0.959977241321462,
24.));
#32352=CARTESIAN_POINT('Ctrl Pts',(-7.7947015489235,0.954033029682695,24.));
#32353=CARTESIAN_POINT('Ctrl Pts',(-7.78767053166018,0.948001590861504,
24.));
#32354=CARTESIAN_POINT('Ctrl Pts',(-7.78071162172877,0.941888233085706,
24.));
#32355=CARTESIAN_POINT('Ctrl Pts',(-7.75269342371654,0.917274425697755,
24.));
#32356=CARTESIAN_POINT('Ctrl Pts',(-7.72591276091907,0.891395901731505,
24.));
#32357=CARTESIAN_POINT('Ctrl Pts',(-7.70047108636338,0.864317009446147,
24.));
#32358=CARTESIAN_POINT('Ctrl Pts',(-7.66652666178374,0.828188199808707,
24.));
#32359=CARTESIAN_POINT('Ctrl Pts',(-7.63496382945612,0.789923205013932,
24.));
#32360=CARTESIAN_POINT('Ctrl Pts',(-7.60593237124235,0.749788275952098,
24.));
#32361=CARTESIAN_POINT('Ctrl Pts',(-7.58573713320593,0.72186909807236,24.));
#32362=CARTESIAN_POINT('Ctrl Pts',(-7.56676769399393,0.693044320670178,
24.));
#32363=CARTESIAN_POINT('Ctrl Pts',(-7.54908818194333,0.663397823661222,
24.));
#32364=CARTESIAN_POINT('Ctrl Pts',(-7.53965734716309,0.647583404445125,
24.));
#32365=CARTESIAN_POINT('Ctrl Pts',(-7.53059376289677,0.631535105539703,
24.));
#32366=CARTESIAN_POINT('Ctrl Pts',(-7.52190861271761,0.615265404204942,
24.));
#32367=CARTESIAN_POINT('Ctrl Pts',(-7.51748915437742,0.606986529830519,
24.));
#32368=CARTESIAN_POINT('Ctrl Pts',(-7.51316770089473,0.59865032588924,24.));
#32369=CARTESIAN_POINT('Ctrl Pts',(-7.50894583197787,0.590258430824365,
24.));
#32370=CARTESIAN_POINT('Ctrl Pts',(-7.50442354109893,0.581269380890268,
24.));
#32371=CARTESIAN_POINT('Ctrl Pts',(-7.50001888167444,0.572222977380615,
24.));
#32372=CARTESIAN_POINT('Ctrl Pts',(-7.49573658730706,0.563128806983175,
24.));
#32373=CARTESIAN_POINT('Ctrl Pts',(-7.47506533165207,0.519229928221484,
24.));
#32374=CARTESIAN_POINT('Ctrl Pts',(-7.45721483404256,0.474166736055567,
24.));
#32375=CARTESIAN_POINT('Ctrl Pts',(-7.44233259800518,0.428186696862096,
24.));
#32376=CARTESIAN_POINT('Ctrl Pts',(-7.43702164425509,0.411778016004576,
24.));
#32377=CARTESIAN_POINT('Ctrl Pts',(-7.43208916293203,0.395252421852314,
24.));
#32378=CARTESIAN_POINT('Ctrl Pts',(-7.42754343322645,0.378620794841048,
24.));
#32379=CARTESIAN_POINT('Ctrl Pts',(-7.4156225733453,0.335005510158975,24.));
#32380=CARTESIAN_POINT('Ctrl Pts',(-7.40635868431464,0.290660713814978,
24.));
#32381=CARTESIAN_POINT('Ctrl Pts',(-7.39978197468916,0.245833679491224,
24.));
#32382=CARTESIAN_POINT('Ctrl Pts',(-7.39701836248096,0.226996822404678,
24.));
#32383=CARTESIAN_POINT('Ctrl Pts',(-7.39472972284664,0.208074861590042,
24.));
#32384=CARTESIAN_POINT('Ctrl Pts',(-7.39292035690482,0.189086585034831,
24.));
#32385=CARTESIAN_POINT('Ctrl Pts',(-7.392030464189,0.17974766215474,24.));
#32386=CARTESIAN_POINT('Ctrl Pts',(-7.39125638738652,0.170390733140474,
24.));
#32387=CARTESIAN_POINT('Ctrl Pts',(-7.39059917635802,0.161024335815622,
24.));
#32388=CARTESIAN_POINT('Ctrl Pts',(-7.3872631549861,0.113480243737833,24.));
#32389=CARTESIAN_POINT('Ctrl Pts',(-7.38694590585192,0.0658798878746482,
24.));
#32390=CARTESIAN_POINT('Ctrl Pts',(-7.38964476207475,0.0185121699340391,
24.));
#32391=CARTESIAN_POINT('Ctrl Pts',(-7.39231303882574,-0.0283188466494503,
24.));
#32392=CARTESIAN_POINT('Ctrl Pts',(-7.39792964052343,-0.0749235404025428,
24.));
#32393=CARTESIAN_POINT('Ctrl Pts',(-7.4065414629921,-0.121013652593743,
24.));
#32394=CARTESIAN_POINT('Ctrl Pts',(-7.40892335149359,-0.133761419824211,
24.));
#32395=CARTESIAN_POINT('Ctrl Pts',(-7.41153465540497,-0.146469716439907,
24.));
#32396=CARTESIAN_POINT('Ctrl Pts',(-7.41437701908526,-0.159132152321132,
24.));
#32397=CARTESIAN_POINT('Ctrl Pts',(-7.41931573092333,-0.18113360217748,
24.));
#32398=CARTESIAN_POINT('Ctrl Pts',(-7.42495191576504,-0.202996694808475,
24.));
#32399=CARTESIAN_POINT('Ctrl Pts',(-7.43127562948781,-0.224689624790342,
24.));
#32400=CARTESIAN_POINT('Ctrl Pts',(-7.43448561573921,-0.235701193315895,
24.));
#32401=CARTESIAN_POINT('Ctrl Pts',(-7.43787279027184,-0.246668889780893,
24.));
#32402=CARTESIAN_POINT('Ctrl Pts',(-7.44143604991943,-0.25758837346045,
24.));
#32403=CARTESIAN_POINT('Ctrl Pts',(-7.44466461678404,-0.267482202895614,
24.));
#32404=CARTESIAN_POINT('Ctrl Pts',(-7.44803514244817,-0.277328343641491,
24.));
#32405=CARTESIAN_POINT('Ctrl Pts',(-7.45154465378086,-0.287119754649393,
24.));
#32406=CARTESIAN_POINT('Ctrl Pts',(-7.46731935144868,-0.331130596544133,
24.));
#32407=CARTESIAN_POINT('Ctrl Pts',(-7.48590745098904,-0.37406509962981,
24.));
#32408=CARTESIAN_POINT('Ctrl Pts',(-7.50719025592286,-0.415648653082733,
24.));
#32409=CARTESIAN_POINT('Ctrl Pts',(-7.51904262814917,-0.438806491325817,
24.));
#32410=CARTESIAN_POINT('Ctrl Pts',(-7.53173151770624,-0.461544875560217,
24.));
#32411=CARTESIAN_POINT('Ctrl Pts',(-7.545241722074,-0.483811700343089,24.));
#32412=CARTESIAN_POINT('Ctrl Pts',(-7.55097545041931,-0.493261736844557,
24.));
#32413=CARTESIAN_POINT('Ctrl Pts',(-7.55685657402864,-0.502625594711996,
24.));
#32414=CARTESIAN_POINT('Ctrl Pts',(-7.56287708030514,-0.511889163975369,
24.));
#32415=CARTESIAN_POINT('Ctrl Pts',(-7.5881701579766,-0.550806850650343,
24.));
#32416=CARTESIAN_POINT('Ctrl Pts',(-7.61595032929573,-0.588007881425946,
24.));
#32417=CARTESIAN_POINT('Ctrl Pts',(-7.64611624065442,-0.623205040740634,
24.));
#32418=CARTESIAN_POINT('Ctrl Pts',(-7.66532287318705,-0.645615068308218,
24.));
#32419=CARTESIAN_POINT('Ctrl Pts',(-7.68549754918253,-0.667211980957074,
24.));
#32420=CARTESIAN_POINT('Ctrl Pts',(-7.7065805280024,-0.687941579884204,
24.));
#32421=CARTESIAN_POINT('Ctrl Pts',(-7.70661869325984,-0.687936125025627,
22.8));
#32422=CARTESIAN_POINT('Ctrl Pts',(-7.67409887424617,-0.655902278122709,
22.8));
#32423=CARTESIAN_POINT('Ctrl Pts',(-7.64381509977965,-0.621808637047501,
22.8));
#32424=CARTESIAN_POINT('Ctrl Pts',(-7.61585772416164,-0.585954657403442,
22.8));
#32425=CARTESIAN_POINT('Ctrl Pts',(-7.58750148055764,-0.549589148893234,
22.8));
#32426=CARTESIAN_POINT('Ctrl Pts',(-7.5615377630002,-0.511411926505863,
22.8));
#32427=CARTESIAN_POINT('Ctrl Pts',(-7.53809119922464,-0.471690207387441,
22.8));
#32428=CARTESIAN_POINT('Ctrl Pts',(-7.51732937629883,-0.436516810273061,
22.8));
#32429=CARTESIAN_POINT('Ctrl Pts',(-7.49854136850491,-0.400131309259636,
22.8));
#32430=CARTESIAN_POINT('Ctrl Pts',(-7.48184017620086,-0.362698053565758,
22.8));
#32431=CARTESIAN_POINT('Ctrl Pts',(-7.47711294155032,-0.352102655334479,
22.8));
#32432=CARTESIAN_POINT('Ctrl Pts',(-7.4725517371607,-0.341419507353799,
22.8));
#32433=CARTESIAN_POINT('Ctrl Pts',(-7.46816951388458,-0.330677896224689,
22.8));
#32434=CARTESIAN_POINT('Ctrl Pts',(-7.45706946072126,-0.303469685442133,
22.8));
#32435=CARTESIAN_POINT('Ctrl Pts',(-7.44710318825052,-0.275857043294133,
22.8));
#32436=CARTESIAN_POINT('Ctrl Pts',(-7.43829808473137,-0.247908606918607,
22.8));
#32437=CARTESIAN_POINT('Ctrl Pts',(-7.42417847687612,-0.203091307390929,
22.8));
#32438=CARTESIAN_POINT('Ctrl Pts',(-7.41304200334992,-0.157411667924642,
22.8));
#32439=CARTESIAN_POINT('Ctrl Pts',(-7.40485337567042,-0.111173146702142,
22.8));
#32440=CARTESIAN_POINT('Ctrl Pts',(-7.3990667072828,-0.0784977095566693,
22.8));
#32441=CARTESIAN_POINT('Ctrl Pts',(-7.39475310628434,-0.0455424363337794,
22.8));
#32442=CARTESIAN_POINT('Ctrl Pts',(-7.39191475620744,-0.0124086226667018,
22.8));
#32443=CARTESIAN_POINT('Ctrl Pts',(-7.39015601726076,0.00812222341272933,
22.8));
#32444=CARTESIAN_POINT('Ctrl Pts',(-7.38896393745883,0.028721696174667,
22.8));
#32445=CARTESIAN_POINT('Ctrl Pts',(-7.38834146456221,0.0493660552932196,
22.8));
#32446=CARTESIAN_POINT('Ctrl Pts',(-7.38797934168981,0.0613758868268767,
22.8));
#32447=CARTESIAN_POINT('Ctrl Pts',(-7.38781020265733,0.0734053336283251,
22.8));
#32448=CARTESIAN_POINT('Ctrl Pts',(-7.38783436635261,0.0854208914751402,
22.8));
#32449=CARTESIAN_POINT('Ctrl Pts',(-7.38793158368919,0.133762857296808,
22.8));
#32450=CARTESIAN_POINT('Ctrl Pts',(-7.39114907770623,0.181961184367851,
22.8));
#32451=CARTESIAN_POINT('Ctrl Pts',(-7.39745467436063,0.229704925733033,
22.8));
#32452=CARTESIAN_POINT('Ctrl Pts',(-7.3999312816523,0.248456917729558,22.8));
#32453=CARTESIAN_POINT('Ctrl Pts',(-7.40288481096348,0.267138971151595,
22.8));
#32454=CARTESIAN_POINT('Ctrl Pts',(-7.40631544490045,0.285732738634787,
22.8));
#32455=CARTESIAN_POINT('Ctrl Pts',(-7.41475540033853,0.33147663666289,22.8));
#32456=CARTESIAN_POINT('Ctrl Pts',(-7.42607978052882,0.37668661873272,22.8));
#32457=CARTESIAN_POINT('Ctrl Pts',(-7.44015842069487,0.421132678936863,
22.8));
#32458=CARTESIAN_POINT('Ctrl Pts',(-7.44619862362351,0.440201510858501,
22.8));
#32459=CARTESIAN_POINT('Ctrl Pts',(-7.45274637533637,0.459129659953141,
22.8));
#32460=CARTESIAN_POINT('Ctrl Pts',(-7.45979389453231,0.477898384958879,
22.8));
#32461=CARTESIAN_POINT('Ctrl Pts',(-7.46424271571329,0.489746341526856,
22.8));
#32462=CARTESIAN_POINT('Ctrl Pts',(-7.4688928540224,0.501535475997375,22.8));
#32463=CARTESIAN_POINT('Ctrl Pts',(-7.47373027012052,0.513232377204913,
22.8));
#32464=CARTESIAN_POINT('Ctrl Pts',(-7.49246848990274,0.558541505291551,
22.8));
#32465=CARTESIAN_POINT('Ctrl Pts',(-7.51403747741391,0.602540157612762,
22.8));
#32466=CARTESIAN_POINT('Ctrl Pts',(-7.53825727973114,0.64497438097173,22.8));
#32467=CARTESIAN_POINT('Ctrl Pts',(-7.56269818112947,0.687795980233644,
22.8));
#32468=CARTESIAN_POINT('Ctrl Pts',(-7.58983884034064,0.729025540060729,
22.8));
#32469=CARTESIAN_POINT('Ctrl Pts',(-7.61954520807962,0.768390367753865,
22.8));
#32470=CARTESIAN_POINT('Ctrl Pts',(-7.624943127649,0.775543318111749,22.8));
#32471=CARTESIAN_POINT('Ctrl Pts',(-7.63042588898144,0.78263464183452,22.8));
#32472=CARTESIAN_POINT('Ctrl Pts',(-7.6359928529246,0.789662617571405,22.8));
#32473=CARTESIAN_POINT('Ctrl Pts',(-7.65117021204093,0.808823171278727,
22.8));
#32474=CARTESIAN_POINT('Ctrl Pts',(-7.66697325962642,0.827513014577617,
22.8));
#32475=CARTESIAN_POINT('Ctrl Pts',(-7.68337375414277,0.845711485231679,
22.8));
#32476=CARTESIAN_POINT('Ctrl Pts',(-7.69112592074004,0.854313517090244,
22.8));
#32477=CARTESIAN_POINT('Ctrl Pts',(-7.69901160789439,0.862805734908379,
22.8));
#32478=CARTESIAN_POINT('Ctrl Pts',(-7.70702801425658,0.871185789564867,
22.8));
#32479=CARTESIAN_POINT('Ctrl Pts',(-7.71445567795972,0.878950394425205,
22.8));
#32480=CARTESIAN_POINT('Ctrl Pts',(-7.72198985783713,0.886612666880794,
22.8));
#32481=CARTESIAN_POINT('Ctrl Pts',(-7.72962396642253,0.894167421350373,
22.8));
#32482=CARTESIAN_POINT('Ctrl Pts',(-7.76528195653565,0.929454758066893,
22.8));
#32483=CARTESIAN_POINT('Ctrl Pts',(-7.80314189130454,0.962425220262479,
22.8));
#32484=CARTESIAN_POINT('Ctrl Pts',(-7.84293242203276,0.992923281459069,
22.8));
#32485=CARTESIAN_POINT('Ctrl Pts',(-7.86518021716756,1.00997544450119,22.8));
#32486=CARTESIAN_POINT('Ctrl Pts',(-7.88803237641158,1.02625419485435,22.8));
#32487=CARTESIAN_POINT('Ctrl Pts',(-7.91144681261877,1.041727736773,22.8));
#32488=CARTESIAN_POINT('Ctrl Pts',(-7.92363416860997,1.04978180914692,22.8));
#32489=CARTESIAN_POINT('Ctrl Pts',(-7.9359761488319,1.05761880028698,22.8));
#32490=CARTESIAN_POINT('Ctrl Pts',(-7.94844671421418,1.06522202719557,22.8));
#32491=CARTESIAN_POINT('Ctrl Pts',(-7.99400669055524,1.09299966417129,22.8));
#32492=CARTESIAN_POINT('Ctrl Pts',(-8.04133377544581,1.11769811978497,22.8));
#32493=CARTESIAN_POINT('Ctrl Pts',(-8.09012868784477,1.13911684874061,22.8));
#32494=CARTESIAN_POINT('Ctrl Pts',(-8.12124386749461,1.15277498575861,22.8));
#32495=CARTESIAN_POINT('Ctrl Pts',(-8.15295686822968,1.16509867088334,22.8));
#32496=CARTESIAN_POINT('Ctrl Pts',(-8.18517800353954,1.17607954763522,22.8));
#32497=CARTESIAN_POINT('Ctrl Pts',(-9.55016549375182,-1.36966017015294E-5,
23.2841069671524));
#32498=CARTESIAN_POINT('Ctrl Pts',(-9.55006280769147,0.154119316631831,
23.2770974504288));
#32499=CARTESIAN_POINT('Ctrl Pts',(-9.5156733518718,0.308296679411134,23.2700879337053));
#32500=CARTESIAN_POINT('Ctrl Pts',(-9.44996653184482,0.447714329856668,
23.2630784169817));
#32501=CARTESIAN_POINT('Ctrl Pts',(-9.3776186762958,0.601223022428839,23.2553604433654));
#32502=CARTESIAN_POINT('Ctrl Pts',(-9.26730300356168,0.736837678456824,
23.247642469749));
#32503=CARTESIAN_POINT('Ctrl Pts',(-9.1317383100797,0.838922666491548,23.2399244961327));
#32504=CARTESIAN_POINT('Ctrl Pts',(-8.99617361659773,0.941007654526272,
23.2322065225163));
#32505=CARTESIAN_POINT('Ctrl Pts',(-8.8353599023679,1.00956297456774,23.2244885488999));
#32506=CARTESIAN_POINT('Ctrl Pts',(-8.66783811309464,1.03668457141066,23.2167705752836));
#32507=CARTESIAN_POINT('Ctrl Pts',(-8.50031632382139,1.06380616825358,23.2090526016672));
#32508=CARTESIAN_POINT('Ctrl Pts',(-8.3260864595047,1.04949404189796,23.2013346280508));
#32509=CARTESIAN_POINT('Ctrl Pts',(-8.16523627485858,0.995398302717987,
23.1936166544345));
#32510=CARTESIAN_POINT('Ctrl Pts',(-8.00438609021247,0.941302563538019,
23.1858986808181));
#32511=CARTESIAN_POINT('Ctrl Pts',(-7.85691558523692,0.8474232115337,23.1781807072018));
#32512=CARTESIAN_POINT('Ctrl Pts',(-7.73982730631698,0.724584024576948,
23.1704627335854));
#32513=CARTESIAN_POINT('Ctrl Pts',(-7.62273902739704,0.601744837620195,
23.162744759969));
#32514=CARTESIAN_POINT('Ctrl Pts',(-7.5360329745327,0.449945815711004,23.1550267863527));
#32515=CARTESIAN_POINT('Ctrl Pts',(-7.48970588337769,0.286688560209014,
23.1473088127363));
#32516=CARTESIAN_POINT('Ctrl Pts',(-7.44337879222268,0.123431304707024,
23.13959083912));
#32517=CARTESIAN_POINT('Ctrl Pts',(-7.43743066277701,-0.051284184387765,
23.1318728655036));
#32518=CARTESIAN_POINT('Ctrl Pts',(-7.47254728234041,-0.21731416377441,
23.1241548918872));
#32519=CARTESIAN_POINT('Ctrl Pts',(-7.50766390190381,-0.383344143161055,
23.1164369182709));
#32520=CARTESIAN_POINT('Ctrl Pts',(-7.58384527047628,-0.540688612839554,
23.1087189446545));
#32521=CARTESIAN_POINT('Ctrl Pts',(-7.69230809025561,-0.671206609198054,
23.1010009710381));
#32522=CARTESIAN_POINT('Ctrl Pts',(-7.80077091003495,-0.801724605556554,
23.0932829974218));
#32523=CARTESIAN_POINT('Ctrl Pts',(-7.94151518102115,-0.905416128595054,
23.0855650238054));
#32524=CARTESIAN_POINT('Ctrl Pts',(-8.09831385678209,-0.970326116650706,
23.077847050189));
#32525=CARTESIAN_POINT('Ctrl Pts',(-8.25511253254303,-1.03523610470636,
23.0701290765727));
#32526=CARTESIAN_POINT('Ctrl Pts',(-8.42796561307872,-1.06136455777916,
23.0624111029563));
#32527=CARTESIAN_POINT('Ctrl Pts',(-8.59694407560669,-1.04569899349385,
23.05469312934));
#32528=CARTESIAN_POINT('Ctrl Pts',(-8.76592253813466,-1.03003342920854,
23.0469751557236));
#32529=CARTESIAN_POINT('Ctrl Pts',(-8.93102638265491,-0.97257384756512,
23.0392571821072));
#32530=CARTESIAN_POINT('Ctrl Pts',(-9.07322004306799,-0.879945055895734,
23.0315392084909));
#32531=CARTESIAN_POINT('Ctrl Pts',(-9.21541370348107,-0.787316264226347,
23.0238212348745));
#32532=CARTESIAN_POINT('Ctrl Pts',(-9.33469717978697,-0.659518262530998,
23.0161032612582));
#32533=CARTESIAN_POINT('Ctrl Pts',(-9.41731771909817,-0.511285397707312,
23.0083852876418));
#32534=CARTESIAN_POINT('Ctrl Pts',(-9.49993825840937,-0.363052532883626,
23.0006673140254));
#32535=CARTESIAN_POINT('Ctrl Pts',(-9.54589586072586,-0.194384804931602,
22.9929493404091));
#32536=CARTESIAN_POINT('Ctrl Pts',(-9.54989190461633,-0.0247288290775425,
22.9852313667927));
#32537=CARTESIAN_POINT('Ctrl Pts',(-9.55008596031612,-0.0164900033739872,
22.9848565669126));
#32538=CARTESIAN_POINT('Ctrl Pts',(-9.55018105960925,-0.00824884712159311,
22.9844817670325));
#32539=CARTESIAN_POINT('Ctrl Pts',(-9.5501777037735,-7.61342713928581E-6,
22.9841069671524));
#32540=CARTESIAN_POINT('Ctrl Pts',(-8.81478889550448,1.17604951161381,22.8));
#32541=CARTESIAN_POINT('Ctrl Pts',(-9.00489125583834,1.12516550422183,22.8077179736164));
#32542=CARTESIAN_POINT('Ctrl Pts',(-9.35978561312172,0.929509121580238,
22.8231539208491));
#32543=CARTESIAN_POINT('Ctrl Pts',(-9.69399222430856,0.421517693774337,
22.8463078416982));
#32544=CARTESIAN_POINT('Ctrl Pts',(-9.75281474611789,-0.183635193835607,
22.8694617625473));
#32545=CARTESIAN_POINT('Ctrl Pts',(-9.5227777403229,-0.746471923361528,
22.8926156833964));
#32546=CARTESIAN_POINT('Ctrl Pts',(-9.05688665443706,-1.13717116763217,
22.9157696042454));
#32547=CARTESIAN_POINT('Ctrl Pts',(-8.46258911977101,-1.2656564697317,22.9389235250945));
#32548=CARTESIAN_POINT('Ctrl Pts',(-7.87691550790518,-1.10229307735719,
22.9620774459436));
#32549=CARTESIAN_POINT('Ctrl Pts',(-7.43491956993902,-0.684753972836506,
22.9852313667927));
#32550=CARTESIAN_POINT('Ctrl Pts',(-7.23851903592649,-0.109317603314454,
23.0083852876418));
#32551=CARTESIAN_POINT('Ctrl Pts',(-7.33300252317075,0.49132599619855,23.0315392084909));
#32552=CARTESIAN_POINT('Ctrl Pts',(-7.69658280697753,0.978675268097788,
23.05469312934));
#32553=CARTESIAN_POINT('Ctrl Pts',(-8.24542239893397,1.24035263469515,23.077847050189));
#32554=CARTESIAN_POINT('Ctrl Pts',(-8.85296478970154,1.21601821059452,23.1010009710381));
#32555=CARTESIAN_POINT('Ctrl Pts',(-9.37911735435305,0.911283219057196,
23.1241548918872));
#32556=CARTESIAN_POINT('Ctrl Pts',(-9.70255502492968,0.396416244609647,
23.1473088127363));
#32557=CARTESIAN_POINT('Ctrl Pts',(-9.74869660384231,-0.209860001191851,
23.1704627335854));
#32558=CARTESIAN_POINT('Ctrl Pts',(-9.50690234210182,-0.767744815010462,
23.1936166544345));
#32559=CARTESIAN_POINT('Ctrl Pts',(-9.03292736505941,-1.14859603498855,
23.2167705752836));
#32560=CARTESIAN_POINT('Ctrl Pts',(-8.436065140539,-1.2645935163393,23.2399244961327));
#32561=CARTESIAN_POINT('Ctrl Pts',(-7.85394559851473,-1.08898950325348,
23.2630784169817));
#32562=CARTESIAN_POINT('Ctrl Pts',(-7.42079916644579,-0.662276368844085,
23.2862323378308));
#32563=CARTESIAN_POINT('Ctrl Pts',(-7.23650469503931,-0.0828495154220059,
23.3093862586799));
#32564=CARTESIAN_POINT('Ctrl Pts',(-7.34355848256139,0.515681534104197,
23.332540179529));
#32565=CARTESIAN_POINT('Ctrl Pts',(-7.71727509134788,0.995302037194035,
23.3556941003781));
#32566=CARTESIAN_POINT('Ctrl Pts',(-8.27147954086117,1.24541672849857,23.3788480212272));
#32567=CARTESIAN_POINT('Ctrl Pts',(-8.87837831986,1.20835188373602,23.4020019420763));
#32568=CARTESIAN_POINT('Ctrl Pts',(-9.39802717851571,0.892654252505216,
23.4251558629254));
#32569=CARTESIAN_POINT('Ctrl Pts',(-9.7106007485556,0.371120270889709,23.4483097837744));
#32570=CARTESIAN_POINT('Ctrl Pts',(-9.74402296838762,-0.235990004009924,
23.4714637046235));
#32571=CARTESIAN_POINT('Ctrl Pts',(-9.49058703805816,-0.788683553714432,
23.4946176254726));
#32572=CARTESIAN_POINT('Ctrl Pts',(-9.0087325233999,-1.15951526402384,23.5177715463217));
#32573=CARTESIAN_POINT('Ctrl Pts',(-8.40956982850905,-1.26297538057999,
23.5409254671708));
#32574=CARTESIAN_POINT('Ctrl Pts',(-7.8312593464559,-1.07520712710119,23.5640793880199));
#32575=CARTESIAN_POINT('Ctrl Pts',(-7.40715317709645,-0.639507818195355,
23.587233308869));
#32576=CARTESIAN_POINT('Ctrl Pts',(-7.23504558492588,-0.0563449701204428,
23.6103872297181));
#32577=CARTESIAN_POINT('Ctrl Pts',(-7.35462270660441,0.539810414542498,
23.6335411505671));
#32578=CARTESIAN_POINT('Ctrl Pts',(-7.73831135994277,1.011491395628,23.6566950714162));
#32579=CARTESIAN_POINT('Ctrl Pts',(-8.2976371195735,1.24993347528822,23.6798489922653));
#32580=CARTESIAN_POINT('Ctrl Pts',(-8.90362555579596,1.20015450597578,23.7030029131144));
#32581=CARTESIAN_POINT('Ctrl Pts',(-9.41654233415426,0.873632976856196,
23.7261568339635));
#32582=CARTESIAN_POINT('Ctrl Pts',(-9.71811443025979,0.345661195055098,
23.7493107548126));
#32583=CARTESIAN_POINT('Ctrl Pts',(-9.73880260375737,-0.262016291447522,
23.7724646756616));
#32584=CARTESIAN_POINT('Ctrl Pts',(-9.47383638460599,-0.809275680645407,
23.7956185965108));
#32585=CARTESIAN_POINT('Ctrl Pts',(-8.98431410313225,-1.16992489625058,
23.8187725173598));
#32586=CARTESIAN_POINT('Ctrl Pts',(-8.38311425495986,-1.2608022005996,23.8419264382089));
#32587=CARTESIAN_POINT('Ctrl Pts',(-7.80886700439182,-1.06095217981207,
23.865080359058));
#32588=CARTESIAN_POINT('Ctrl Pts',(-7.39398745671621,-0.616458283433,23.8882342799071));
#32589=CARTESIAN_POINT('Ctrl Pts',(-7.23414244016268,-0.0298154996095495,
23.9113882007562));
#32590=CARTESIAN_POINT('Ctrl Pts',(-7.36619019624783,0.563701731054729,
23.9345421216053));
#32591=CARTESIAN_POINT('Ctrl Pts',(-7.75968252106489,1.02723702411681,23.9576960424544));
#32592=CARTESIAN_POINT('Ctrl Pts',(-8.32388300007083,1.25389944282625,23.9808499633035));
#32593=CARTESIAN_POINT('Ctrl Pts',(-8.92869574141285,1.19143384195749,24.0040038841525));
#32594=CARTESIAN_POINT('Ctrl Pts',(-9.43465056894933,0.854221860214417,
24.0271578050016));
#32595=CARTESIAN_POINT('Ctrl Pts',(-9.72509085321044,0.320073427910269,
24.0503117258507));
#32596=CARTESIAN_POINT('Ctrl Pts',(-9.73300691540701,-0.287945227761225,
24.0734656466998));
#32597=CARTESIAN_POINT('Ctrl Pts',(-9.54874216054247,-0.648885562186029,
24.0889015939325));
#32598=CARTESIAN_POINT('Ctrl Pts',(-9.41981913331181,-0.797569598526366,
24.0966195675489));
#32599=CARTESIAN_POINT('Ctrl Pts',(-8.80036532666177,1.12216314098433,22.7677934774837));
#32600=CARTESIAN_POINT('Ctrl Pts',(-8.98175723208253,1.07361062937918,22.7755114511001));
#32601=CARTESIAN_POINT('Ctrl Pts',(-9.32039039569844,0.886919185923345,
22.7909473983328));
#32602=CARTESIAN_POINT('Ctrl Pts',(-9.63928372190927,0.402203831178163,
22.8141013191819));
#32603=CARTESIAN_POINT('Ctrl Pts',(-9.69541100667265,-0.175221063292699,
22.837255240031));
#32604=CARTESIAN_POINT('Ctrl Pts',(-9.47591425384351,-0.712268718199221,
22.8604091608801));
#32605=CARTESIAN_POINT('Ctrl Pts',(-9.03137021115533,-1.08506619551744,
22.8835630817292));
#32606=CARTESIAN_POINT('Ctrl Pts',(-8.46430327936862,-1.20766432489081,
22.9067170025782));
#32607=CARTESIAN_POINT('Ctrl Pts',(-7.90546512383795,-1.05178621287385,
22.9298709234273));
#32608=CARTESIAN_POINT('Ctrl Pts',(-7.48372135782099,-0.65337867272721,
22.9530248442764));
#32609=CARTESIAN_POINT('Ctrl Pts',(-7.29631985987209,-0.104308690993709,
22.9761787651255));
#32610=CARTESIAN_POINT('Ctrl Pts',(-7.38647413124429,0.468813530124974,
22.9993326859746));
#32611=CARTESIAN_POINT('Ctrl Pts',(-7.73339523384031,0.933832548720903,
23.0224866068237));
#32612=CARTESIAN_POINT('Ctrl Pts',(-8.25708709742628,1.18351990688532,23.0456405276727));
#32613=CARTESIAN_POINT('Ctrl Pts',(-8.83679200846301,1.16030048158635,23.0687944485218));
#32614=CARTESIAN_POINT('Ctrl Pts',(-9.33883636012989,0.869528390875553,
23.0919483693709));
#32615=CARTESIAN_POINT('Ctrl Pts',(-9.64745417659313,0.378252525761392,
23.11510229022));
#32616=CARTESIAN_POINT('Ctrl Pts',(-9.6914815569128,-0.200244254836913,
23.1382562110691));
#32617=CARTESIAN_POINT('Ctrl Pts',(-9.46076626342624,-0.732566889895946,
23.1614101319182));
#32618=CARTESIAN_POINT('Ctrl Pts',(-9.00850873197586,-1.09596757756927,
23.1845640527673));
#32619=CARTESIAN_POINT('Ctrl Pts',(-8.43899462394853,-1.20665007582583,
23.2077179736164));
#32620=CARTESIAN_POINT('Ctrl Pts',(-7.88354769143807,-1.03909220606962,
23.2308718944654));
#32621=CARTESIAN_POINT('Ctrl Pts',(-7.47024794859846,-0.63193098838327,
23.2540258153145));
#32622=CARTESIAN_POINT('Ctrl Pts',(-7.29439781571098,-0.079053365982365,
23.2771797361636));
#32623=CARTESIAN_POINT('Ctrl Pts',(-7.3965464185323,0.492053101798328,23.3003336570127));
#32624=CARTESIAN_POINT('Ctrl Pts',(-7.75313940157635,0.9496974823391,23.3234875778618));
#32625=CARTESIAN_POINT('Ctrl Pts',(-8.28195030594033,1.18835196484935,23.3466414987109));
#32626=CARTESIAN_POINT('Ctrl Pts',(-8.86104109538026,1.15298542440347,23.36979541956));
#32627=CARTESIAN_POINT('Ctrl Pts',(-9.35687973965453,0.851753000117917,
23.3929493404091));
#32628=CARTESIAN_POINT('Ctrl Pts',(-9.65513124665388,0.354115608868437,
23.4161032612581));
#32629=CARTESIAN_POINT('Ctrl Pts',(-9.68702206656833,-0.225176985769323,
23.4392571821073));
#32630=CARTESIAN_POINT('Ctrl Pts',(-9.44519852358965,-0.752546219473707,
23.4624111029563));
#32631=CARTESIAN_POINT('Ctrl Pts',(-8.98542249347644,-1.10638648955414,
23.4855650238054));
#32632=CARTESIAN_POINT('Ctrl Pts',(-8.41371332220462,-1.20510608274707,
23.5087189446545));
#32633=CARTESIAN_POINT('Ctrl Pts',(-7.86190091924345,-1.02594133583792,
23.5318728655036));
#32634=CARTESIAN_POINT('Ctrl Pts',(-7.45722721595169,-0.610205688504884,
23.5550267863527));
#32635=CARTESIAN_POINT('Ctrl Pts',(-7.29300556175248,-0.0537632540336343,
23.5781807072018));
#32636=CARTESIAN_POINT('Ctrl Pts',(-7.40710368188054,0.51507640140748,23.6013346280508));
#32637=CARTESIAN_POINT('Ctrl Pts',(-7.7732117922435,0.965145047370478,23.6244885488999));
#32638=CARTESIAN_POINT('Ctrl Pts',(-8.30690934924464,1.19266175513832,23.647642469749));
#32639=CARTESIAN_POINT('Ctrl Pts',(-8.88513150764547,1.14516364897274,23.6707963905981));
#32640=CARTESIAN_POINT('Ctrl Pts',(-9.3745465342937,0.83360327579335,23.6939503114472));
#32641=CARTESIAN_POINT('Ctrl Pts',(-9.66230065285511,0.329823063169471,
23.7171042322963));
#32642=CARTESIAN_POINT('Ctrl Pts',(-9.68204089807779,-0.250010753540766,
23.7402581531454));
#32643=CARTESIAN_POINT('Ctrl Pts',(-9.42921538197376,-0.772194818965664,
23.7634120739945));
#32644=CARTESIAN_POINT('Ctrl Pts',(-8.96212292069925,-1.11631915436179,
23.7865659948435));
#32645=CARTESIAN_POINT('Ctrl Pts',(-8.38846993813164,-1.20303247747056,
23.8097199156926));
#32646=CARTESIAN_POINT('Ctrl Pts',(-7.8405345901421,-1.0123395475913,23.8328738365417));
#32647=CARTESIAN_POINT('Ctrl Pts',(-7.44466474643886,-0.588212279152875,
23.8560277573908));
#32648=CARTESIAN_POINT('Ctrl Pts',(-7.29214379891493,-0.0284493589440447,
23.8791816782399));
#32649=CARTESIAN_POINT('Ctrl Pts',(-7.41814115129264,0.537873022225616,
23.902335599089));
#32650=CARTESIAN_POINT('Ctrl Pts',(-7.79360373072436,0.98016921408055,23.9254895199381));
#32651=CARTESIAN_POINT('Ctrl Pts',(-8.33195264836252,1.19644600277889,23.9486434407872));
#32652=CARTESIAN_POINT('Ctrl Pts',(-8.90905298200441,1.1368425641633,23.9717973616362));
#32653=CARTESIAN_POINT('Ctrl Pts',(-9.391825053127,0.815081572918051,23.9949512824853));
#32654=CARTESIAN_POINT('Ctrl Pts',(-9.66895741739932,0.305407722772266,
24.0181052033344));
#32655=CARTESIAN_POINT('Ctrl Pts',(-9.67651076709336,-0.274751630798765,
24.0412591241835));
#32656=CARTESIAN_POINT('Ctrl Pts',(-9.50068898914138,-0.619153746004165,
24.0566950714162));
#32657=CARTESIAN_POINT('Ctrl Pts',(-9.37767319112124,-0.761025107359477,
24.0644130450326));
#32658=CARTESIAN_POINT('Ctrl Pts',(-8.78594175781906,1.06827677035485,22.7355869549674));
#32659=CARTESIAN_POINT('Ctrl Pts',(-8.95862320832672,1.02205575453654,22.7433049285838));
#32660=CARTESIAN_POINT('Ctrl Pts',(-9.28099517827516,0.844329250266453,
22.7587408758165));
#32661=CARTESIAN_POINT('Ctrl Pts',(-9.58457521950998,0.38288996858199,22.7818947966656));
#32662=CARTESIAN_POINT('Ctrl Pts',(-9.63800726722741,-0.166806932749792,
22.8050487175147));
#32663=CARTESIAN_POINT('Ctrl Pts',(-9.42905076736411,-0.678065513036913,
22.8282026383638));
#32664=CARTESIAN_POINT('Ctrl Pts',(-9.0058537678736,-1.03296122340271,22.8513565592129));
#32665=CARTESIAN_POINT('Ctrl Pts',(-8.46601743896623,-1.14967218004993,
22.8745104800619));
#32666=CARTESIAN_POINT('Ctrl Pts',(-7.93401473977073,-1.00127934839051,
22.897664400911));
#32667=CARTESIAN_POINT('Ctrl Pts',(-7.53252314570295,-0.622003372617913,
22.9208183217601));
#32668=CARTESIAN_POINT('Ctrl Pts',(-7.35412068381769,-0.0992997786729641,
22.9439722426092));
#32669=CARTESIAN_POINT('Ctrl Pts',(-7.43994573931782,0.446301064051396,
22.9671261634583));
#32670=CARTESIAN_POINT('Ctrl Pts',(-7.77020766070311,0.888989829344018,
22.9902800843074));
#32671=CARTESIAN_POINT('Ctrl Pts',(-8.26875179591859,1.12668717907549,23.0134340051565));
#32672=CARTESIAN_POINT('Ctrl Pts',(-8.82061922722448,1.10458275257818,23.0365879260056));
#32673=CARTESIAN_POINT('Ctrl Pts',(-9.29855536590672,0.827773562693911,
23.0597418468546));
#32674=CARTESIAN_POINT('Ctrl Pts',(-9.59235332825659,0.360088806913137,
23.0828957677037));
#32675=CARTESIAN_POINT('Ctrl Pts',(-9.63426650998328,-0.190628508481975,
23.1060496885528));
#32676=CARTESIAN_POINT('Ctrl Pts',(-9.41463018475067,-0.697388964781431,
23.1292036094019));
#32677=CARTESIAN_POINT('Ctrl Pts',(-8.98409009889231,-1.04333912014998,
23.152357530251));
#32678=CARTESIAN_POINT('Ctrl Pts',(-8.44192410735806,-1.14870663531236,
23.1755114511001));
#32679=CARTESIAN_POINT('Ctrl Pts',(-7.91314978436141,-0.98919490888576,
23.1986653719492));
#32680=CARTESIAN_POINT('Ctrl Pts',(-7.51969673075113,-0.601585607922455,
23.2218192927983));
#32681=CARTESIAN_POINT('Ctrl Pts',(-7.35229093638265,-0.075257216542724,
23.2449732136473));
#32682=CARTESIAN_POINT('Ctrl Pts',(-7.44953435450321,0.468424669492461,
23.2681271344964));
#32683=CARTESIAN_POINT('Ctrl Pts',(-7.78900371180481,0.904092927484164,
23.2912810553455));
#32684=CARTESIAN_POINT('Ctrl Pts',(-8.29242107101949,1.13128720120013,23.3144349761946));
#32685=CARTESIAN_POINT('Ctrl Pts',(-8.84370387090052,1.09761896507093,23.3375888970437));
#32686=CARTESIAN_POINT('Ctrl Pts',(-9.31573230079336,0.81085174773062,23.3607428178928));
#32687=CARTESIAN_POINT('Ctrl Pts',(-9.59966174475214,0.337110946847165,
23.3838967387418));
#32688=CARTESIAN_POINT('Ctrl Pts',(-9.63002116474905,-0.214363967528721,
23.407050659591));
#32689=CARTESIAN_POINT('Ctrl Pts',(-9.39981000912115,-0.716408885232983,
23.43020458044));
#32690=CARTESIAN_POINT('Ctrl Pts',(-8.96211246355297,-1.05325771508445,
23.4533585012891));
#32691=CARTESIAN_POINT('Ctrl Pts',(-8.41785681590019,-1.14723678491415,
23.4765124221382));
#32692=CARTESIAN_POINT('Ctrl Pts',(-7.892542492031,-0.976675544574657,23.4996663429873));
#32693=CARTESIAN_POINT('Ctrl Pts',(-7.50730125480692,-0.580903558814412,
23.5228202638364));
#32694=CARTESIAN_POINT('Ctrl Pts',(-7.35096553857909,-0.0511815379468251,
23.5459741846855));
#32695=CARTESIAN_POINT('Ctrl Pts',(-7.45958465715666,0.49034238827246,23.5691281055345));
#32696=CARTESIAN_POINT('Ctrl Pts',(-7.80811222454424,0.918798699112961,
23.5922820263836));
#32697=CARTESIAN_POINT('Ctrl Pts',(-8.31618157891577,1.13539003498842,23.6154359472327));
#32698=CARTESIAN_POINT('Ctrl Pts',(-8.86663745949497,1.09017279196971,23.6385898680818));
#32699=CARTESIAN_POINT('Ctrl Pts',(-9.33255073443314,0.793573574730505,
23.6617437889309));
#32700=CARTESIAN_POINT('Ctrl Pts',(-9.60648687545043,0.313984931283844,
23.68489770978));
#32701=CARTESIAN_POINT('Ctrl Pts',(-9.62527919239822,-0.238005215634009,
23.7080516306291));
#32702=CARTESIAN_POINT('Ctrl Pts',(-9.38459437934153,-0.735113957285921,
23.7312055514782));
#32703=CARTESIAN_POINT('Ctrl Pts',(-8.93993173826624,-1.062713412473,23.7543594723273));
#32704=CARTESIAN_POINT('Ctrl Pts',(-8.39382562130343,-1.14526275434153,
23.7775133931763));
#32705=CARTESIAN_POINT('Ctrl Pts',(-7.87220217589238,-0.963726915370522,
23.8006673140254));
#32706=CARTESIAN_POINT('Ctrl Pts',(-7.49534203616152,-0.559966274872751,
23.8238212348745));
#32707=CARTESIAN_POINT('Ctrl Pts',(-7.35014515766718,-0.0270832182785388,
23.8469751557236));
#32708=CARTESIAN_POINT('Ctrl Pts',(-7.47009210633745,0.512044313396504,
23.8701290765727));
#32709=CARTESIAN_POINT('Ctrl Pts',(-7.82752494038384,0.933101404044286,
23.8932829974218));
#32710=CARTESIAN_POINT('Ctrl Pts',(-8.34002229665421,1.13899256273153,23.9164369182709));
#32711=CARTESIAN_POINT('Ctrl Pts',(-8.88941022259596,1.08225128636912,23.9395908391199));
#32712=CARTESIAN_POINT('Ctrl Pts',(-9.34899953730467,0.775941285621684,
23.962744759969));
#32713=CARTESIAN_POINT('Ctrl Pts',(-9.61282398158819,0.290742017634264,
23.9858986808181));
#32714=CARTESIAN_POINT('Ctrl Pts',(-9.62001461877971,-0.261558033836305,
24.0090526016672));
#32715=CARTESIAN_POINT('Ctrl Pts',(-9.45263581774029,-0.5894219298223,24.0244885488999));
#32716=CARTESIAN_POINT('Ctrl Pts',(-9.33552724893067,-0.724480616192588,
24.0322065225163));
#32717=CARTESIAN_POINT('Ctrl Pts',(-8.77151818897635,1.01439039972537,22.7033804324511));
#32718=CARTESIAN_POINT('Ctrl Pts',(-8.9354891845709,0.9705008796939,22.7110984060675));
#32719=CARTESIAN_POINT('Ctrl Pts',(-9.24159996085188,0.801739314609559,
22.7265343533002));
#32720=CARTESIAN_POINT('Ctrl Pts',(-9.5298667171107,0.363576105985816,22.7496882741493));
#32721=CARTESIAN_POINT('Ctrl Pts',(-9.58060352778217,-0.158392802206884,
22.7728421949984));
#32722=CARTESIAN_POINT('Ctrl Pts',(-9.38218728088471,-0.643862307874607,
22.7959961158475));
#32723=CARTESIAN_POINT('Ctrl Pts',(-8.98033732459186,-0.980856251287975,
22.8191500366966));
#32724=CARTESIAN_POINT('Ctrl Pts',(-8.46773159856383,-1.09168003520905,
22.8423039575456));
#32725=CARTESIAN_POINT('Ctrl Pts',(-7.96256435570351,-0.950772483907168,
22.8654578783947));
#32726=CARTESIAN_POINT('Ctrl Pts',(-7.58132493358492,-0.590628072508616,
22.8886117992438));
#32727=CARTESIAN_POINT('Ctrl Pts',(-7.41192150776329,-0.0942908663522186,
22.9117657200929));
#32728=CARTESIAN_POINT('Ctrl Pts',(-7.49341734739136,0.42378859797782,22.934919640942));
#32729=CARTESIAN_POINT('Ctrl Pts',(-7.8070200875659,0.844147109967134,22.9580735617911));
#32730=CARTESIAN_POINT('Ctrl Pts',(-8.28041649441091,1.06985445126566,22.9812274826402));
#32731=CARTESIAN_POINT('Ctrl Pts',(-8.80444644598594,1.04886502357001,23.0043814034893));
#32732=CARTESIAN_POINT('Ctrl Pts',(-9.25827437168355,0.786018734512268,
23.0275353243383));
#32733=CARTESIAN_POINT('Ctrl Pts',(-9.53725247992004,0.341925088064882,
23.0506892451874));
#32734=CARTESIAN_POINT('Ctrl Pts',(-9.57705146305377,-0.181012762127038,
23.0738431660365));
#32735=CARTESIAN_POINT('Ctrl Pts',(-9.36849410607509,-0.662211039666914,
23.0969970868856));
#32736=CARTESIAN_POINT('Ctrl Pts',(-8.95967146580877,-0.990710662730691,
23.1201510077347));
#32737=CARTESIAN_POINT('Ctrl Pts',(-8.44485359076759,-1.09076319479888,
23.1433049285838));
#32738=CARTESIAN_POINT('Ctrl Pts',(-7.94275187728475,-0.9392976117019,23.1664588494329));
#32739=CARTESIAN_POINT('Ctrl Pts',(-7.56914551290379,-0.57124022746164,
23.189612770282));
#32740=CARTESIAN_POINT('Ctrl Pts',(-7.41018405705432,-0.071461067103083,
23.212766691131));
#32741=CARTESIAN_POINT('Ctrl Pts',(-7.50252229047412,0.444796237186593,
23.2359206119801));
#32742=CARTESIAN_POINT('Ctrl Pts',(-7.82486802203328,0.858488372629229,
23.2590745328292));
#32743=CARTESIAN_POINT('Ctrl Pts',(-8.30289183609866,1.07422243755091,23.2822284536783));
#32744=CARTESIAN_POINT('Ctrl Pts',(-8.82636664642078,1.04225250573838,23.3053823745274));
#32745=CARTESIAN_POINT('Ctrl Pts',(-9.27458486193219,0.769950495343321,
23.3285362953765));
#32746=CARTESIAN_POINT('Ctrl Pts',(-9.54419224285041,0.320106284825893,
23.3516902162256));
#32747=CARTESIAN_POINT('Ctrl Pts',(-9.57302026292976,-0.203550949288119,
23.3748441370746));
#32748=CARTESIAN_POINT('Ctrl Pts',(-9.35442149465265,-0.680271550992258,
23.3979980579237));
#32749=CARTESIAN_POINT('Ctrl Pts',(-8.9388024336295,-1.00012894061475,23.4211519787728));
#32750=CARTESIAN_POINT('Ctrl Pts',(-8.42200030959576,-1.08936748708124,
23.4443058996219));
#32751=CARTESIAN_POINT('Ctrl Pts',(-7.92318406481855,-0.927409753311392,
23.467459820471));
#32752=CARTESIAN_POINT('Ctrl Pts',(-7.55737529366215,-0.551601429123941,
23.4906137413201));
#32753=CARTESIAN_POINT('Ctrl Pts',(-7.40892551540569,-0.0485998218600163,
23.5137676621692));
#32754=CARTESIAN_POINT('Ctrl Pts',(-7.51206563243278,0.465608375137441,
23.5369215830183));
#32755=CARTESIAN_POINT('Ctrl Pts',(-7.84301265684497,0.872452350855443,
23.5600755038674));
#32756=CARTESIAN_POINT('Ctrl Pts',(-8.32545380858691,1.07811831483852,23.5832294247164));
#32757=CARTESIAN_POINT('Ctrl Pts',(-8.84814341134448,1.03518193496667,23.6063833455655));
#32758=CARTESIAN_POINT('Ctrl Pts',(-9.29055493457258,0.753543873667659,
23.6295372664146));
#32759=CARTESIAN_POINT('Ctrl Pts',(-9.55067309804575,0.298146799398216,
23.6526911872637));
#32760=CARTESIAN_POINT('Ctrl Pts',(-9.56851748671864,-0.225999677727252,
23.6758451081128));
#32761=CARTESIAN_POINT('Ctrl Pts',(-9.33997337670931,-0.698033095606178,
23.6989990289619));
#32762=CARTESIAN_POINT('Ctrl Pts',(-8.91774055583324,-1.0091076705842,23.722152949811));
#32763=CARTESIAN_POINT('Ctrl Pts',(-8.39918130447521,-1.08749303121249,
23.74530687066));
#32764=CARTESIAN_POINT('Ctrl Pts',(-7.90386976164266,-0.915114283149746,
23.7684607915091));
#32765=CARTESIAN_POINT('Ctrl Pts',(-7.54601932588418,-0.531720270592626,
23.7916147123582));
#32766=CARTESIAN_POINT('Ctrl Pts',(-7.40814651641942,-0.0257170776130338,
23.8147686332073));
#32767=CARTESIAN_POINT('Ctrl Pts',(-7.52204306138227,0.486215604567391,
23.8379225540564));
#32768=CARTESIAN_POINT('Ctrl Pts',(-7.86144615004332,0.886033594008022,
23.8610764749055));
#32769=CARTESIAN_POINT('Ctrl Pts',(-8.3480919449459,1.08153912268417,23.8842303957546));
#32770=CARTESIAN_POINT('Ctrl Pts',(-8.86976746318751,1.02766000857494,23.9073843166037));
#32771=CARTESIAN_POINT('Ctrl Pts',(-9.30617402148235,0.736800998325318,
23.9305382374527));
#32772=CARTESIAN_POINT('Ctrl Pts',(-9.55669054577707,0.276076312496261,
23.9536921583018));
#32773=CARTESIAN_POINT('Ctrl Pts',(-9.56351847046606,-0.248364436873845,
23.9768460791509));
#32774=CARTESIAN_POINT('Ctrl Pts',(-9.40458264633919,-0.559690113640436,
23.9922820263836));
#32775=CARTESIAN_POINT('Ctrl Pts',(-9.2933813067401,-0.687936125025699,
24.));
#32776=CARTESIAN_POINT('Ctrl Pts',(-9.2933813067401,-0.687936125025699,
24.));
#32777=CARTESIAN_POINT('Ctrl Pts',(-9.32590110166393,-0.655902301852627,
24.));
#32778=CARTESIAN_POINT('Ctrl Pts',(-9.35618485076755,-0.621808682852868,
24.));
#32779=CARTESIAN_POINT('Ctrl Pts',(-9.38414220215367,-0.585954725174177,
24.));
#32780=CARTESIAN_POINT('Ctrl Pts',(-9.41249843269251,-0.549589224178562,
24.));
#32781=CARTESIAN_POINT('Ctrl Pts',(-9.43846213639955,-0.511412007721187,
24.));
#32782=CARTESIAN_POINT('Ctrl Pts',(-9.4619086878745,-0.471690294888102,
24.));
#32783=CARTESIAN_POINT('Ctrl Pts',(-9.48267051934571,-0.436516870409484,
24.));
#32784=CARTESIAN_POINT('Ctrl Pts',(-9.50145853320447,-0.400131340040127,
24.));
#32785=CARTESIAN_POINT('Ctrl Pts',(-9.51815973041198,-0.362698054803428,
24.));
#32786=CARTESIAN_POINT('Ctrl Pts',(-9.52288697181288,-0.352102636190975,
24.));
#32787=CARTESIAN_POINT('Ctrl Pts',(-9.52744818249553,-0.34141946758306,
24.));
#32788=CARTESIAN_POINT('Ctrl Pts',(-9.53183041159058,-0.330677835735727,
24.));
#32789=CARTESIAN_POINT('Ctrl Pts',(-9.54293046193044,-0.303469615523773,
24.));
#32790=CARTESIAN_POINT('Ctrl Pts',(-9.55289673212501,-0.275856964651056,
24.));
#32791=CARTESIAN_POINT('Ctrl Pts',(-9.56170183443649,-0.2479085208202,24.));
#32792=CARTESIAN_POINT('Ctrl Pts',(-9.57582144309734,-0.203091200633333,
24.));
#32793=CARTESIAN_POINT('Ctrl Pts',(-9.58695791901247,-0.157411543429852,
24.));
#32794=CARTESIAN_POINT('Ctrl Pts',(-9.59514654937063,-0.111173006432213,
24.));
#32795=CARTESIAN_POINT('Ctrl Pts',(-9.60093321692656,-0.0784975735239973,
24.));
#32796=CARTESIAN_POINT('Ctrl Pts',(-9.60524681862521,-0.0455423057826866,
24.));
#32797=CARTESIAN_POINT('Ctrl Pts',(-9.60808517048093,-0.0124084983709903,
24.));
#32798=CARTESIAN_POINT('Ctrl Pts',(-9.60984391284602,0.00812237087063378,
24.));
#32799=CARTESIAN_POINT('Ctrl Pts',(-9.61103599498872,0.0287218666781537,
24.));
#32800=CARTESIAN_POINT('Ctrl Pts',(-9.61165846902993,0.0493662487424586,
24.));
#32801=CARTESIAN_POINT('Ctrl Pts',(-9.6120205910809,0.0613760442993463,
24.));
#32802=CARTESIAN_POINT('Ctrl Pts',(-9.61218973047166,0.0734054549032458,
24.));
#32803=CARTESIAN_POINT('Ctrl Pts',(-9.61216556829573,0.0854209765709245,
24.));
#32804=CARTESIAN_POINT('Ctrl Pts',(-9.61206835676509,0.133762949416384,
24.));
#32805=CARTESIAN_POINT('Ctrl Pts',(-9.60885086759177,0.181961282887962,
24.));
#32806=CARTESIAN_POINT('Ctrl Pts',(-9.60254527348847,0.229705031101198,
24.));
#32807=CARTESIAN_POINT('Ctrl Pts',(-9.60006866958979,0.248457007683516,
24.));
#32808=CARTESIAN_POINT('Ctrl Pts',(-9.59711514423865,0.267139045895045,
24.));
#32809=CARTESIAN_POINT('Ctrl Pts',(-9.59368451474868,0.285732798488276,
24.));
#32810=CARTESIAN_POINT('Ctrl Pts',(-9.58524456415484,0.331476692924977,
24.));
#32811=CARTESIAN_POINT('Ctrl Pts',(-9.57392018758713,0.376686672569883,
24.));
#32812=CARTESIAN_POINT('Ctrl Pts',(-9.55984155019052,0.421132731117061,
24.));
#32813=CARTESIAN_POINT('Ctrl Pts',(-9.55380134842738,0.440201562399408,
24.));
#32814=CARTESIAN_POINT('Ctrl Pts',(-9.54725359771895,0.45912971099526,24.));
#32815=CARTESIAN_POINT('Ctrl Pts',(-9.54020607939479,0.477898435611738,
24.));
#32816=CARTESIAN_POINT('Ctrl Pts',(-9.53575725876718,0.489746391925897,
24.));
#32817=CARTESIAN_POINT('Ctrl Pts',(-9.53110712095903,0.501535526186162,
24.));
#32818=CARTESIAN_POINT('Ctrl Pts',(-9.52626970531564,0.513232427219491,
24.));
#32819=CARTESIAN_POINT('Ctrl Pts',(-9.50753148918547,0.55854155005979,24.));
#32820=CARTESIAN_POINT('Ctrl Pts',(-9.4859625052079,0.602540197938336,24.));
#32821=CARTESIAN_POINT('Ctrl Pts',(-9.4617427066771,0.644974417278716,24.));
#32822=CARTESIAN_POINT('Ctrl Pts',(-9.43730180712568,0.687796015944042,
24.));
#32823=CARTESIAN_POINT('Ctrl Pts',(-9.41016114958247,0.729025575350205,
24.));
#32824=CARTESIAN_POINT('Ctrl Pts',(-9.38045478374864,0.768390402360951,
24.));
#32825=CARTESIAN_POINT('Ctrl Pts',(-9.37505686111558,0.775543357113344,
24.));
#32826=CARTESIAN_POINT('Ctrl Pts',(-9.36957409662013,0.782634685144143,
24.));
#32827=CARTESIAN_POINT('Ctrl Pts',(-9.36400712941827,0.789662665096707,
24.));
#32828=CARTESIAN_POINT('Ctrl Pts',(-9.34882977059882,0.808823218706664,
24.));
#32829=CARTESIAN_POINT('Ctrl Pts',(-9.33302672335631,0.827513061791383,
24.));
#32830=CARTESIAN_POINT('Ctrl Pts',(-9.31662622921216,0.845711532137706,
24.));
#32831=CARTESIAN_POINT('Ctrl Pts',(-9.30887406128153,0.854313565525556,
24.));
#32832=CARTESIAN_POINT('Ctrl Pts',(-9.30098837274836,0.86280578480931,24.));
#32833=CARTESIAN_POINT('Ctrl Pts',(-9.29297196496173,0.871185840868798,
24.));
#32834=CARTESIAN_POINT('Ctrl Pts',(-9.28554430284086,0.878950443995364,
24.));
#32835=CARTESIAN_POINT('Ctrl Pts',(-9.27801012459867,0.886612714734314,
24.));
#32836=CARTESIAN_POINT('Ctrl Pts',(-9.27037601768741,0.894167467518663,
24.));
#32837=CARTESIAN_POINT('Ctrl Pts',(-9.23471802897501,0.929454802715901,
24.));
#32838=CARTESIAN_POINT('Ctrl Pts',(-9.19685809573334,0.962425263167257,
24.));
#32839=CARTESIAN_POINT('Ctrl Pts',(-9.15706756650192,0.992923322602774,
24.));
#32840=CARTESIAN_POINT('Ctrl Pts',(-9.1348197718603,1.00997548492369,24.));
#32841=CARTESIAN_POINT('Ctrl Pts',(-9.11196761308139,1.02625423452634,24.));
#32842=CARTESIAN_POINT('Ctrl Pts',(-9.08855317728612,1.04172777569958,24.));
#32843=CARTESIAN_POINT('Ctrl Pts',(-9.0763658218002,1.04978184749329,24.));
#32844=CARTESIAN_POINT('Ctrl Pts',(-9.06402384207715,1.05761883806443,24.));
#32845=CARTESIAN_POINT('Ctrl Pts',(-9.05155327718193,1.06522206442192,24.));
#32846=CARTESIAN_POINT('Ctrl Pts',(-9.00599330223546,1.09299969961885,24.));
#32847=CARTESIAN_POINT('Ctrl Pts',(-8.95866621855187,1.11769815363806,24.));
#32848=CARTESIAN_POINT('Ctrl Pts',(-8.90987130699021,1.13911688142547,24.));
#32849=CARTESIAN_POINT('Ctrl Pts',(-8.87875612767952,1.15277501778401,24.));
#32850=CARTESIAN_POINT('Ctrl Pts',(-8.84704312712587,1.16509870240582,24.));
#32851=CARTESIAN_POINT('Ctrl Pts',(-8.81482199187078,1.17607957877115,24.));
#32852=CARTESIAN_POINT('Ctrl Pts',(-9.55005297345142,-1.9100363332081E-5,
23.0658930328476));
#32853=CARTESIAN_POINT('Ctrl Pts',(-9.55009366141186,-0.0583092414421507,
23.0685430772439));
#32854=CARTESIAN_POINT('Ctrl Pts',(-9.5453162224635,-0.116592782065231,
23.0711931216402));
#32855=CARTESIAN_POINT('Ctrl Pts',(-9.5356587397017,-0.174056166685031,
23.0738431660365));
#32856=CARTESIAN_POINT('Ctrl Pts',(-9.50753234406088,-0.341412187973663,
23.0815611396529));
#32857=CARTESIAN_POINT('Ctrl Pts',(-9.43801322506799,-0.501811613820288,
23.0892791132692));
#32858=CARTESIAN_POINT('Ctrl Pts',(-9.33511655886048,-0.636761263920897,
23.0969970868856));
#32859=CARTESIAN_POINT('Ctrl Pts',(-9.23221989265299,-0.771710914021506,
23.104715060502));
#32860=CARTESIAN_POINT('Ctrl Pts',(-9.09594567923088,-0.881210788376099,
23.1124330341183));
#32861=CARTESIAN_POINT('Ctrl Pts',(-8.94200559334629,-0.952636147564761,
23.1201510077347));
#32862=CARTESIAN_POINT('Ctrl Pts',(-8.78806550746171,-1.02406150675342,
23.127868981351));
#32863=CARTESIAN_POINT('Ctrl Pts',(-8.61645954911465,-1.05741235077615,
23.1355869549674));
#32864=CARTESIAN_POINT('Ctrl Pts',(-8.44697295102731,-1.04884350893802,
23.1433049285838));
#32865=CARTESIAN_POINT('Ctrl Pts',(-8.27748635293998,-1.04027466709989,
23.1510229022002));
#32866=CARTESIAN_POINT('Ctrl Pts',(-8.11011911511237,-0.989786139400895,
23.1587408758165));
#32867=CARTESIAN_POINT('Ctrl Pts',(-7.96416776880173,-0.903198978178021,
23.1664588494329));
#32868=CARTESIAN_POINT('Ctrl Pts',(-7.8182164224911,-0.816611816955147,
23.1741768230492));
#32869=CARTESIAN_POINT('Ctrl Pts',(-7.69368096769745,-0.693926022208393,
23.1818947966656));
#32870=CARTESIAN_POINT('Ctrl Pts',(-7.60491966432571,-0.54928659810859,
23.189612770282));
#32871=CARTESIAN_POINT('Ctrl Pts',(-7.51615836095397,-0.404647174008787,
23.1973307438983));
#32872=CARTESIAN_POINT('Ctrl Pts',(-7.46317120900415,-0.238054120555935,
23.2050487175147));
#32873=CARTESIAN_POINT('Ctrl Pts',(-7.4520673385992,-0.0687147097812286,
23.212766691131));
#32874=CARTESIAN_POINT('Ctrl Pts',(-7.44096346819426,0.100624700993478,
23.2204846647474));
#32875=CARTESIAN_POINT('Ctrl Pts',(-7.47174287933419,0.272710469090037,
23.2282026383638));
#32876=CARTESIAN_POINT('Ctrl Pts',(-7.54085687349735,0.427702042378756,
23.2359206119801));
#32877=CARTESIAN_POINT('Ctrl Pts',(-7.60997086766051,0.582693615667473,
23.2436385855965));
#32878=CARTESIAN_POINT('Ctrl Pts',(-7.71741944484689,0.720590994148351,
23.2513565592129));
#32879=CARTESIAN_POINT('Ctrl Pts',(-7.85081436911765,0.825495360875735,
23.2590745328292));
#32880=CARTESIAN_POINT('Ctrl Pts',(-7.9842092933884,0.930399727603121,23.2667925064456));
#32881=CARTESIAN_POINT('Ctrl Pts',(-8.14355056474353,1.00231108257701,23.2745104800619));
#32882=CARTESIAN_POINT('Ctrl Pts',(-8.31046700214145,1.03293843809521,23.2822284536783));
#32883=CARTESIAN_POINT('Ctrl Pts',(-8.47738343953937,1.0635657936134,23.2899464272947));
#32884=CARTESIAN_POINT('Ctrl Pts',(-8.65187504298008,1.05290914967589,23.297664400911));
#32885=CARTESIAN_POINT('Ctrl Pts',(-8.813823880619,1.00219715930796,23.3053823745274));
#32886=CARTESIAN_POINT('Ctrl Pts',(-8.97577271825792,0.951485168940026,
23.3131003481438));
#32887=CARTESIAN_POINT('Ctrl Pts',(-9.12517879009505,0.860717832141674,
23.3208183217601));
#32888=CARTESIAN_POINT('Ctrl Pts',(-9.24481638949999,0.740360128656261,
23.3285362953765));
#32889=CARTESIAN_POINT('Ctrl Pts',(-9.36445398890493,0.620002425170845,
23.3362542689928));
#32890=CARTESIAN_POINT('Ctrl Pts',(-9.45432311587767,0.470054354998369,
23.3439722426092));
#32891=CARTESIAN_POINT('Ctrl Pts',(-9.50406234937726,0.307804114226461,
23.3516902162256));
#32892=CARTESIAN_POINT('Ctrl Pts',(-9.53457282822537,0.208278404020019,
23.3564244884329));
#32893=CARTESIAN_POINT('Ctrl Pts',(-9.54998362241142,0.104123753125398,
23.3611587606403));
#32894=CARTESIAN_POINT('Ctrl Pts',(-9.55003901931283,-1.48519368357603E-5,
23.3658930328476));
#32895=CARTESIAN_POINT('Ctrl Pts',(-8.81478889550448,1.17604951161381,22.8));
#32896=CARTESIAN_POINT('Ctrl Pts',(-8.86280031082267,1.1596387533803,22.8));
#32897=CARTESIAN_POINT('Ctrl Pts',(-8.90960753249362,1.1402211917786,22.8));
#32898=CARTESIAN_POINT('Ctrl Pts',(-8.95497271964666,1.11798779949959,22.8));
#32899=CARTESIAN_POINT('Ctrl Pts',(-9.00031627609065,1.0957650083901,22.8));
#32900=CARTESIAN_POINT('Ctrl Pts',(-9.04422007096444,1.07072837077275,22.8));
#32901=CARTESIAN_POINT('Ctrl Pts',(-9.08641936496114,1.04302434852895,22.8));
#32902=CARTESIAN_POINT('Ctrl Pts',(-9.125198107991,1.01756593305001,22.8));
#32903=CARTESIAN_POINT('Ctrl Pts',(-9.16253770006956,0.989854158189036,
22.8));
#32904=CARTESIAN_POINT('Ctrl Pts',(-9.19820266623766,0.959977147630981,
22.8));
#32905=CARTESIAN_POINT('Ctrl Pts',(-9.20529843014922,0.954032933011403,
22.8));
#32906=CARTESIAN_POINT('Ctrl Pts',(-9.21232944776528,0.948001491271412,
22.8));
#32907=CARTESIAN_POINT('Ctrl Pts',(-9.21928835806176,0.941888130657366,
22.8));
#32908=CARTESIAN_POINT('Ctrl Pts',(-9.24730655571085,0.917274313452249,
22.8));
#32909=CARTESIAN_POINT('Ctrl Pts',(-9.27408721843744,0.89139578122503,22.8));
#32910=CARTESIAN_POINT('Ctrl Pts',(-9.29952889345206,0.864316883517271,
22.8));
#32911=CARTESIAN_POINT('Ctrl Pts',(-9.33347331898954,0.828188066277435,
22.8));
#32912=CARTESIAN_POINT('Ctrl Pts',(-9.36503615316936,0.789923068886875,
22.8));
#32913=CARTESIAN_POINT('Ctrl Pts',(-9.39406761371715,0.749788140423142,
22.8));
#32914=CARTESIAN_POINT('Ctrl Pts',(-9.41426285222677,0.721868964549862,
22.8));
#32915=CARTESIAN_POINT('Ctrl Pts',(-9.43323229228493,0.69304419080465,22.8));
#32916=CARTESIAN_POINT('Ctrl Pts',(-9.45091180542575,0.663397698483226,
22.8));
#32917=CARTESIAN_POINT('Ctrl Pts',(-9.46034264350897,0.64758327720412,22.8));
#32918=CARTESIAN_POINT('Ctrl Pts',(-9.46940623093581,0.63153497639394,22.8));
#32919=CARTESIAN_POINT('Ctrl Pts',(-9.47809138410351,0.615265273228403,
22.8));
#32920=CARTESIAN_POINT('Ctrl Pts',(-9.48251083054356,0.6069864230634,22.8));
#32921=CARTESIAN_POINT('Ctrl Pts',(-9.48683227267676,0.598650243698863,
22.8));
#32922=CARTESIAN_POINT('Ctrl Pts',(-9.49105413080523,0.590258373551913,
22.8));
#32923=CARTESIAN_POINT('Ctrl Pts',(-9.49557643033991,0.581269310133437,
22.8));
#32924=CARTESIAN_POINT('Ctrl Pts',(-9.49998109806241,0.572222892914978,
22.8));
#32925=CARTESIAN_POINT('Ctrl Pts',(-9.5042634003018,0.563128708694731,22.8));
#32926=CARTESIAN_POINT('Ctrl Pts',(-9.52493465811296,0.519229839327299,
22.8));
#32927=CARTESIAN_POINT('Ctrl Pts',(-9.54278515814712,0.47416665717555,22.8));
#32928=CARTESIAN_POINT('Ctrl Pts',(-9.55766739651793,0.428186626834186,
22.8));
#32929=CARTESIAN_POINT('Ctrl Pts',(-9.56297835233027,0.411777945336887,
22.8));
#32930=CARTESIAN_POINT('Ctrl Pts',(-9.56791083552882,0.395252350342727,
22.8));
#32931=CARTESIAN_POINT('Ctrl Pts',(-9.57245656690096,0.378620722213359,
22.8));
#32932=CARTESIAN_POINT('Ctrl Pts',(-9.58437742872468,0.335005443481923,
22.8));
#32933=CARTESIAN_POINT('Ctrl Pts',(-9.59364131934433,0.29066065148619,22.8));
#32934=CARTESIAN_POINT('Ctrl Pts',(-9.60021803028088,0.245833620405334,
22.8));
#32935=CARTESIAN_POINT('Ctrl Pts',(-9.60298164316936,0.226996763799839,
22.8));
#32936=CARTESIAN_POINT('Ctrl Pts',(-9.6052702833904,0.208074803263039,22.8));
#32937=CARTESIAN_POINT('Ctrl Pts',(-9.60707964983028,0.189086526821981,
22.8));
#32938=CARTESIAN_POINT('Ctrl Pts',(-9.60796954273001,0.179747604638758,
22.8));
#32939=CARTESIAN_POINT('Ctrl Pts',(-9.60874361971098,0.170390676282926,
22.8));
#32940=CARTESIAN_POINT('Ctrl Pts',(-9.60940083091284,0.161024279585984,
22.8));
#32941=CARTESIAN_POINT('Ctrl Pts',(-9.61273685317894,0.113480190493206,
22.8));
#32942=CARTESIAN_POINT('Ctrl Pts',(-9.6130541030529,0.0658798367366342,
22.8));
#32943=CARTESIAN_POINT('Ctrl Pts',(-9.6103552475085,0.0185121206120323,
22.8));
#32944=CARTESIAN_POINT('Ctrl Pts',(-9.60768697144596,-0.0283188938653337,
22.8));
#32945=CARTESIAN_POINT('Ctrl Pts',(-9.60207037041557,-0.0749235858009301,
22.8));
#32946=CARTESIAN_POINT('Ctrl Pts',(-9.5934585486852,-0.121013695903488,
22.8));
#32947=CARTESIAN_POINT('Ctrl Pts',(-9.59107666009507,-0.133761464123487,
22.8));
#32948=CARTESIAN_POINT('Ctrl Pts',(-9.58846535604412,-0.146469761698218,
22.8));
#32949=CARTESIAN_POINT('Ctrl Pts',(-9.5856229921747,-0.159132198493557,
22.8));
#32950=CARTESIAN_POINT('Ctrl Pts',(-9.58068428043452,-0.181133648038205,
22.8));
#32951=CARTESIAN_POINT('Ctrl Pts',(-9.57504809566159,-0.202996740245752,
22.8));
#32952=CARTESIAN_POINT('Ctrl Pts',(-9.56872438197767,-0.224689669718014,
22.8));
#32953=CARTESIAN_POINT('Ctrl Pts',(-9.565514395063,-0.235701240327858,22.8));
#32954=CARTESIAN_POINT('Ctrl Pts',(-9.56212721978399,-0.246668938836283,
22.8));
#32955=CARTESIAN_POINT('Ctrl Pts',(-9.55856395930746,-0.257588424518991,
22.8));
#32956=CARTESIAN_POINT('Ctrl Pts',(-9.55533539309684,-0.267482251463418,
22.8));
#32957=CARTESIAN_POINT('Ctrl Pts',(-9.55196486814714,-0.27732838971353,
22.8));
#32958=CARTESIAN_POINT('Ctrl Pts',(-9.54845535758285,-0.287119798241869,
22.8));
#32959=CARTESIAN_POINT('Ctrl Pts',(-9.53268065995049,-0.331130638528512,
22.8));
#32960=CARTESIAN_POINT('Ctrl Pts',(-9.51409256034865,-0.374065139761816,
22.8));
#32961=CARTESIAN_POINT('Ctrl Pts',(-9.49280975524792,-0.415648691358816,
22.8));
#32962=CARTESIAN_POINT('Ctrl Pts',(-9.48095738273575,-0.438806528945255,
22.8));
#32963=CARTESIAN_POINT('Ctrl Pts',(-9.46826849283286,-0.461544912508254,
22.8));
#32964=CARTESIAN_POINT('Ctrl Pts',(-9.45475828805827,-0.48381173664456,
22.8));
#32965=CARTESIAN_POINT('Ctrl Pts',(-9.44902455967591,-0.493261772648128,
22.8));
#32966=CARTESIAN_POINT('Ctrl Pts',(-9.44314343602737,-0.502625630023286,
22.8));
#32967=CARTESIAN_POINT('Ctrl Pts',(-9.43712292970736,-0.511889198807362,
22.8));
#32968=CARTESIAN_POINT('Ctrl Pts',(-9.41182985269796,-0.550806882168746,
22.8));
#32969=CARTESIAN_POINT('Ctrl Pts',(-9.38404968213532,-0.588007909962575,
22.8));
#32970=CARTESIAN_POINT('Ctrl Pts',(-9.35388377160583,-0.62320506690565,
22.8));
#32971=CARTESIAN_POINT('Ctrl Pts',(-9.33467713894622,-0.645615093727404,
22.8));
#32972=CARTESIAN_POINT('Ctrl Pts',(-9.31450246278731,-0.667212005822818,
22.8));
#32973=CARTESIAN_POINT('Ctrl Pts',(-9.29341948377037,-0.687941604344758,
22.8));
#32974=CARTESIAN_POINT('Origin',(-8.5,0.,24.));
#32975=CARTESIAN_POINT('',(-7.46076951545867,-1.8,24.));
#32976=CARTESIAN_POINT('',(-6.42153903091735,0.,24.));
#32977=CARTESIAN_POINT('',(-7.46076951545867,-1.8,24.));
#32978=CARTESIAN_POINT('',(-7.46076951545867,1.8,24.));
#32979=CARTESIAN_POINT('',(-6.42153903091735,0.,24.));
#32980=CARTESIAN_POINT('',(-9.53923048454133,1.8,24.));
#32981=CARTESIAN_POINT('',(-7.46076951545867,1.8,24.));
#32982=CARTESIAN_POINT('',(-10.5784609690827,2.22044604925031E-16,24.));
#32983=CARTESIAN_POINT('',(-9.53923048454133,1.8,24.));
#32984=CARTESIAN_POINT('',(-9.53923048454133,-1.8,24.));
#32985=CARTESIAN_POINT('',(-10.5784609690827,2.54538057293978E-16,24.));
#32986=CARTESIAN_POINT('',(-9.53923048454133,-1.8,24.));
#32987=CARTESIAN_POINT('Origin',(-8.5,0.,22.7));
#32988=CARTESIAN_POINT('Origin',(-9.53923048454133,-1.8,22.8));
#32989=CARTESIAN_POINT('',(-9.53923048454133,-1.8,22.8));
#32990=CARTESIAN_POINT('',(-7.46076951545867,-1.8,22.8));
#32991=CARTESIAN_POINT('',(-9.53923048454133,-1.8,22.8));
#32992=CARTESIAN_POINT('',(-7.46076951545867,-1.8,22.8));
#32993=CARTESIAN_POINT('',(-9.53923048454133,-1.8,22.8));
#32994=CARTESIAN_POINT('Origin',(-10.5784609690827,2.54538057293978E-16,
22.8));
#32995=CARTESIAN_POINT('',(-10.5784609690827,2.54538057293978E-16,22.8));
#32996=CARTESIAN_POINT('',(-10.5784609690827,2.54538057293978E-16,22.8));
#32997=CARTESIAN_POINT('',(-10.5784609690827,2.54538057293978E-16,22.8));
#32998=CARTESIAN_POINT('Origin',(-9.53923048454133,1.8,22.8));
#32999=CARTESIAN_POINT('',(-9.53923048454133,1.8,22.8));
#33000=CARTESIAN_POINT('',(-9.53923048454133,1.8,22.8));
#33001=CARTESIAN_POINT('',(-9.53923048454133,1.8,22.8));
#33002=CARTESIAN_POINT('Origin',(-7.46076951545867,1.8,22.8));
#33003=CARTESIAN_POINT('',(-7.46076951545867,1.8,22.8));
#33004=CARTESIAN_POINT('',(-7.46076951545867,1.8,22.8));
#33005=CARTESIAN_POINT('',(-7.46076951545867,1.8,22.8));
#33006=CARTESIAN_POINT('Origin',(-6.42153903091735,0.,22.8));
#33007=CARTESIAN_POINT('',(-6.42153903091735,0.,22.8));
#33008=CARTESIAN_POINT('',(-6.42153903091735,0.,22.8));
#33009=CARTESIAN_POINT('',(-6.42153903091735,0.,22.8));
#33010=CARTESIAN_POINT('Origin',(-7.46076951545867,-1.8,22.8));
#33011=CARTESIAN_POINT('',(-7.46076951545867,-1.8,22.8));
#33012=CARTESIAN_POINT('Origin',(-8.5,0.,22.8));
#34401=UNCERTAINTY_MEASURE_WITH_UNIT(LENGTH_MEASURE(0.001),#34434,
'DISTANCE_ACCURACY_VALUE',
'Maximum model space distance between geometric entities at asserted c
onnectivities');
#34404=UNCERTAINTY_MEASURE_WITH_UNIT(LENGTH_MEASURE(0.001),#34434,
'DISTANCE_ACCURACY_VALUE',
'Maximum model space distance between geometric entities at asserted c
onnectivities');
#34430=(
GEOMETRIC_REPRESENTATION_CONTEXT(3)
GLOBAL_UNCERTAINTY_ASSIGNED_CONTEXT((#34401))
GLOBAL_UNIT_ASSIGNED_CONTEXT((#34434,#34436,#34437))
REPRESENTATION_CONTEXT('','3D')
);
#34433=(
GEOMETRIC_REPRESENTATION_CONTEXT(3)
GLOBAL_UNCERTAINTY_ASSIGNED_CONTEXT((#34404))
GLOBAL_UNIT_ASSIGNED_CONTEXT((#34434,#34436,#34437))
REPRESENTATION_CONTEXT('','3D')
);
#34434=(
LENGTH_UNIT()
NAMED_UNIT(*)
SI_UNIT(.CENTI.,.METRE.)
);
#34436=(
NAMED_UNIT(*)
PLANE_ANGLE_UNIT()
SI_UNIT($,.RADIAN.)
);
#34437=(
NAMED_UNIT(*)
SI_UNIT($,.STERADIAN.)
SOLID_ANGLE_UNIT()
);
#34463=SHAPE_DEFINITION_REPRESENTATION(#34527,#34562);
#34527=PRODUCT_DEFINITION_SHAPE('',$,#34591);
#34562=SHAPE_REPRESENTATION('',(#9671),#34430);
#34565=PRODUCT_DEFINITION_CONTEXT('part definition',#34651,'design');
#34591=PRODUCT_DEFINITION('M24 adjustment nut (2)',
'M24 adjustment nut (2)',#34619,#34565);
#34619=PRODUCT_DEFINITION_FORMATION('',$,#34678);
#34651=APPLICATION_CONTEXT(
'Core Data for Automotive Mechanical Design Process');
#34652=PRODUCT_CONTEXT('part definition',#34651,'mechanical');
#34678=PRODUCT('M24 adjustment nut (2)','M24 adjustment nut (2)',
'M24 adjustment nut (2)',(#34652));
#34744=COLOUR_RGB('Black',0.12,0.14,0.17);
#34745=FILL_AREA_STYLE_COLOUR('',#34744);
#34746=FILL_AREA_STYLE('',(#34745));
#34747=SURFACE_STYLE_FILL_AREA(#34746);
#34748=SURFACE_SIDE_STYLE('',(#34747));
#34749=SURFACE_STYLE_USAGE(.BOTH.,#34748);
#34750=PRESENTATION_STYLE_ASSIGNMENT((#34749));
ENDSEC;
END-ISO-10303-21;
